ISO-10303-21;
HEADER;
FILE_DESCRIPTION (('STEP AP214'),
    '1' );
FILE_NAME ('pan head cross recess screw_iso_ISO 7045 - M5 x 16 - Z - 16N.step',
    '2026-10-27T14:18:53',
    ( '' ),
    ( '' ),
    'SwSTEP 2.0',
    'SolidWorks 2026',
    '' );
FILE_SCHEMA (( 'AUTOMOTIVE_DESIGN' ));
ENDSEC;

DATA;
#1=DIRECTION ( 'NONE',  ( -1.000000000000000000, -0.000000000000000000, -0.000000000000000000 ) ) ;
#8=CARTESIAN_POINT ( 'NONE',  ( 2.740000000000000213, -0.9838866223905674557, -0.5150000000000000133 ) ) ;
#14=CARTESIAN_POINT ( 'NONE',  ( 0.000000000000000000, -2.349999999999999201, -0.5150000000000000133 ) ) ;
#27=TOROIDAL_SURFACE ( 'NONE', #1462, 4.300000000000001599, 0.4499999999999985678 ) ;
#29=CARTESIAN_POINT ( 'NONE',  ( 19.70000000000000284, 2.500000000000000000, 0.000000000000000000 ) ) ;
#32=EDGE_LOOP ( 'NONE', ( #2166, #2925, #468, #4500 ) ) ;
#36=CARTESIAN_POINT ( 'NONE',  ( 2.740000000000000213, 0.000000000000000000, 0.8509999999999999787 ) ) ;
#38=SPHERICAL_SURFACE ( 'NONE', #3792, 8.000000000000000000 ) ;
#42=DIRECTION ( 'NONE',  ( -1.000000000000000000, -0.000000000000000000, -0.000000000000000000 ) ) ;
#44=ORIENTED_EDGE ( 'NONE', *, *, #2648, .T. ) ;
#46=CARTESIAN_POINT ( 'NONE',  ( 0.3226060873438392207, -0.5150000000000068967, 2.189154565102729766 ) ) ;
#63=DIRECTION ( 'NONE',  ( 0.000000000000000000, 1.000000000000000000, 3.280956645156627724E-15 ) ) ;
#65=AXIS2_PLACEMENT_3D ( 'NONE', #2300, #5491, #4094 ) ;
#69=LINE ( 'NONE', #156, #3339 ) ;
#73=CARTESIAN_POINT ( 'NONE',  ( 2.740000000000000213, 0.000000000000000000, 0.000000000000000000 ) ) ;
#78=ORIENTED_EDGE ( 'NONE', *, *, #4185, .T. ) ;
#97=EDGE_CURVE ( 'NONE', #4020, #2197, #3211, .T. ) ;
#98=VECTOR ( 'NONE', #2286, 1000.000000000000000 ) ;
#99=EDGE_LOOP ( 'NONE', ( #5298, #5545, #3236, #2859 ) ) ;
#101=CARTESIAN_POINT ( 'NONE',  ( 0.06760930072668806801, -4.837354856632045452E-15, 0.000000000000000000 ) ) ;
#103=CARTESIAN_POINT ( 'NONE',  ( 1.424271237134740131, 0.000000000000000000, 0.000000000000000000 ) ) ;
#109=LINE ( 'NONE', #3376, #1061 ) ;
#110=CARTESIAN_POINT ( 'NONE',  ( 7.345657149124971141, -1.312408941149200814, 2.762944903268657774E-16 ) ) ;
#113=AXIS2_PLACEMENT_3D ( 'NONE', #2260, #4112, #2193 ) ;
#123=CIRCLE ( 'NONE', #1373, 0.8509999999999999787 ) ;
#132=COLOUR_RGB ( '',1.000000000000000000, 0.9490196078431372140, 0.9098039215686274384 ) ;
#135=EDGE_CURVE ( 'NONE', #2028, #5067, #3489, .T. ) ;
#136=CARTESIAN_POINT ( 'NONE',  ( 2.740000000000000213, 0.000000000000000000, 0.000000000000000000 ) ) ;
#140=VERTEX_POINT ( 'NONE', #4746 ) ;
#142=CARTESIAN_POINT ( 'NONE',  ( 2.740000000000000213, -0.9838866223905676778, 0.5149999999999995692 ) ) ;
#143=CARTESIAN_POINT ( 'NONE',  ( 0.06760930072668894231, -0.9010842325122859764, 0.5149999999999992362 ) ) ;
#149=CARTESIAN_POINT ( 'NONE',  ( 2.740000000000000213, 0.000000000000000000, 0.000000000000000000 ) ) ;
#156=CARTESIAN_POINT ( 'NONE',  ( 2.740000000000000213, 0.5150000000000035660, -0.9838866223905657904 ) ) ;
#167=ORIENTED_EDGE ( 'NONE', *, *, #1148, .F. ) ;
#171=VERTEX_POINT ( 'NONE', #3409 ) ;
#174=DIRECTION ( 'NONE',  ( 0.8949343913984706411, 1.487067055422294855E-15, -0.4461977533473793223 ) ) ;
#179=DIRECTION ( 'NONE',  ( 1.000000000000000000, 0.000000000000000000, 0.000000000000000000 ) ) ;
#181=DIRECTION ( 'NONE',  ( 0.000000000000000000, 0.000000000000000000, 1.000000000000000000 ) ) ;
#182=DIRECTION ( 'NONE',  ( -0.8949343913984706411, 0.4461977533473793223, 0.000000000000000000 ) ) ;
#186=DIRECTION ( 'NONE',  ( 0.000000000000000000, 0.000000000000000000, -1.000000000000000000 ) ) ;
#189=MANIFOLD_SOLID_BREP ( 'RecessCore', #1492 ) ;
#192=ORIENTED_EDGE ( 'NONE', *, *, #4630, .T. ) ;
#193=ORIENTED_EDGE ( 'NONE', *, *, #1729, .T. ) ;
#194=( NAMED_UNIT ( * ) SI_UNIT ( $, .STERADIAN. ) SOLID_ANGLE_UNIT ( ) );
#198=EDGE_CURVE ( 'NONE', #4039, #4278, #109, .T. ) ;
#199=VERTEX_POINT ( 'NONE', #3354 ) ;
#206=ORIENTED_EDGE ( 'NONE', *, *, #4724, .F. ) ;
#213=CARTESIAN_POINT ( 'NONE',  ( 0.000000000000000000, -2.349999999999997424, 0.5149999999999992362 ) ) ;
#219=ORIENTED_EDGE ( 'NONE', *, *, #1151, .T. ) ;
#222=VECTOR ( 'NONE', #506, 1000.000000000000000 ) ;
#236=CARTESIAN_POINT ( 'NONE',  ( 3.699999999999998401, 5.817072295949927426E-16, -4.750000000000000000 ) ) ;
#239=CIRCLE ( 'NONE', #3046, 1.037871761867652065 ) ;
#244=ADVANCED_FACE ( 'NONE', ( #1649 ), #3949, .T. ) ;
#247=LINE ( 'NONE', #2084, #1072 ) ;
#249=DIRECTION ( 'NONE',  ( -0.000000000000000000, 0.000000000000000000, -1.000000000000000000 ) ) ;
#257=CARTESIAN_POINT ( 'NONE',  ( 2.740000000000000213, -0.5150000000000022338, 0.6774776749089210792 ) ) ;
#269=DIRECTION ( 'NONE',  ( 0.000000000000000000, 1.000000000000000000, 1.153406566473941260E-16 ) ) ;
#275=DIRECTION ( 'NONE',  ( 0.000000000000000000, 0.000000000000000000, 1.000000000000000000 ) ) ;
#277=ADVANCED_FACE ( 'NONE', ( #3588 ), #323, .T. ) ;
#279=CARTESIAN_POINT ( 'NONE',  ( 19.70000000000000284, 0.000000000000000000, 2.500000000000000000 ) ) ;
#280=EDGE_CURVE ( 'NONE', #2788, #5831, #1766, .T. ) ;
#282=ORIENTED_EDGE ( 'NONE', *, *, #2831, .T. ) ;
#300=DIRECTION ( 'NONE',  ( -1.000000000000000000, -0.000000000000000000, -0.000000000000000000 ) ) ;
#302=CARTESIAN_POINT ( 'NONE',  ( 1.424271237134740131, 0.000000000000000000, 0.000000000000000000 ) ) ;
#304=MECHANICAL_DESIGN_GEOMETRIC_PRESENTATION_REPRESENTATION('',(#5611),#1259);
#308=AXIS2_PLACEMENT_3D ( 'NONE', #4125, #4984, #3159 ) ;
#313=CIRCLE ( 'NONE', #2040, 7.983406227920510467 ) ;
#318=AXIS2_PLACEMENT_3D ( 'NONE', #5107, #1395, #3704 ) ;
#320=EDGE_CURVE ( 'NONE', #2852, #1334, #3202, .T. ) ;
#321=ORIENTED_EDGE ( 'NONE', *, *, #1308, .F. ) ;
#323=PLANE ( 'NONE',  #5550 ) ;
#337=CARTESIAN_POINT ( 'NONE',  ( 2.740000000000000213, -0.5149999999999961275, -0.9838866223905694541 ) ) ;
#341=DIRECTION ( 'NONE',  ( -1.000000000000000000, -0.000000000000000000, -0.000000000000000000 ) ) ;
#342=VERTEX_POINT ( 'NONE', #46 ) ;
#345=DIRECTION ( 'NONE',  ( -0.000000000000000000, 1.000000000000000000, 1.224646799147353207E-16 ) ) ;
#347=CARTESIAN_POINT ( 'NONE',  ( 2.740000000000000213, 0.9838866223909998876, -0.5150000000000000133 ) ) ;
#349=ADVANCED_FACE ( 'NONE', ( #2746 ), #3674, .F. ) ;
#350=ORIENTED_EDGE ( 'NONE', *, *, #5483, .F. ) ;
#359=ADVANCED_FACE ( 'NONE', ( #1881 ), #3735, .T. ) ;
#362=DIRECTION ( 'NONE',  ( 0.000000000000000000, 0.000000000000000000, 1.000000000000000000 ) ) ;
#363=DIRECTION ( 'NONE',  ( 0.000000000000000000, 0.000000000000000000, 1.000000000000000000 ) ) ;
#366=DIRECTION ( 'NONE',  ( -1.000000000000000000, -0.000000000000000000, -0.000000000000000000 ) ) ;
#371=DIRECTION ( 'NONE',  ( -1.000000000000000000, -0.000000000000000000, -0.000000000000000000 ) ) ;
#374=CYLINDRICAL_SURFACE ( 'NONE', #2638, 4.749999999999999112 ) ;
#382=ORIENTED_EDGE ( 'NONE', *, *, #3138, .T. ) ;
#393=DIRECTION ( 'NONE',  ( 0.000000000000000000, 0.000000000000000000, -1.000000000000000000 ) ) ;
#397=SHAPE_REPRESENTATION_RELATIONSHIP ( 'NONE' , 'NONE' ,  #951, #4058 ) ;
#403=AXIS2_PLACEMENT_3D ( 'NONE', #4521, #1, #363 ) ;
#405=EDGE_CURVE ( 'NONE', #1403, #3083, #5296, .T. ) ;
#409=ORIENTED_EDGE ( 'NONE', *, *, #2019, .F. ) ;
#414=DIRECTION ( 'NONE',  ( -1.000000000000000000, -0.000000000000000000, -0.000000000000000000 ) ) ;
#418=FACE_OUTER_BOUND ( 'NONE', #802, .T. ) ;
#420=ORIENTED_EDGE ( 'NONE', *, *, #1641, .T. ) ;
#423=DIRECTION ( 'NONE',  ( -1.000000000000000000, -0.000000000000000000, -0.000000000000000000 ) ) ;
#431=CARTESIAN_POINT ( 'NONE',  ( 1.849560077140108394, 0.7556913915602446741, 0.5149999999999996803 ) ) ;
#432=PRODUCT_DEFINITION_FORMATION_WITH_SPECIFIED_SOURCE ( 'ANY', '', #4798, .NOT_KNOWN. ) ;
#433=EDGE_LOOP ( 'NONE', ( #3649, #3374, #834, #5095, #5451 ) ) ;
#443=CARTESIAN_POINT ( 'NONE',  ( 2.740000000000000213, -0.5150000000000034550, 0.9838866223909985553 ) ) ;
#446=CARTESIAN_POINT ( 'NONE',  ( 0.06760930072668806801, -4.837354856632045452E-15, 0.000000000000000000 ) ) ;
#454=FACE_OUTER_BOUND ( 'NONE', #672, .T. ) ;
#458=EDGE_CURVE ( 'NONE', #1563, #1071, #2378, .T. ) ;
#468=ORIENTED_EDGE ( 'NONE', *, *, #5761, .F. ) ;
#473=DIRECTION ( 'NONE',  ( 0.000000000000000000, 1.000000000000000000, 0.000000000000000000 ) ) ;
#489=DIRECTION ( 'NONE',  ( -0.3090169943749412895, 0.000000000000000000, 0.9510565162951555296 ) ) ;
#491=EDGE_CURVE ( 'NONE', #4174, #2799, #3555, .T. ) ;
#492=AXIS2_PLACEMENT_3D ( 'NONE', #4843, #5206, #1562 ) ;
#496=EDGE_CURVE ( 'NONE', #1071, #4278, #5299, .T. ) ;
#504=DIRECTION ( 'NONE',  ( -1.000000000000000000, -0.000000000000000000, -0.000000000000000000 ) ) ;
#505=PLANE ( 'NONE',  #2514 ) ;
#506=DIRECTION ( 'NONE',  ( 0.000000000000000000, -1.000000000000000000, -1.652937667529658626E-16 ) ) ;
#516=DIRECTION ( 'NONE',  ( 0.000000000000000000, -3.491481338843133355E-15, 1.000000000000000000 ) ) ;
#517=AXIS2_PLACEMENT_3D ( 'NONE', #14, #3233, #5026 ) ;
#521=DIRECTION ( 'NONE',  ( -1.000000000000000000, -0.000000000000000000, -0.000000000000000000 ) ) ;
#537=EDGE_CURVE ( 'NONE', #199, #3078, #839, .T. ) ;
#546=B_SPLINE_CURVE_WITH_KNOTS ( 'NONE', 3,
 ( #5885, #4533, #5083, #2790 ),
 .UNSPECIFIED., .F., .F.,
 ( 4, 4 ),
 ( 0.001586480563516618056, 0.004268227385920363680 ),
 .UNSPECIFIED. ) ;
#553=VERTEX_POINT ( 'NONE', #279 ) ;
#565=EDGE_CURVE ( 'NONE', #3630, #140, #2691, .T. ) ;
#579=DIRECTION ( 'NONE',  ( 0.000000000000000000, 3.490239007934759657E-15, -1.000000000000000000 ) ) ;
#591=CIRCLE ( 'NONE', #1662, 7.983406227920510467 ) ;
#598=CARTESIAN_POINT ( 'NONE',  ( 2.740000000000000213, -0.5150000000000034550, 0.9838866223909985553 ) ) ;
#601=PLANE ( 'NONE',  #5069 ) ;
#606=CIRCLE ( 'NONE', #4981, 4.749999999999999112 ) ;
#612=MECHANICAL_DESIGN_GEOMETRIC_PRESENTATION_REPRESENTATION('',(#2355),#5740);
#616=DIRECTION ( 'NONE',  ( 0.000000000000000000, -1.000000000000000000, -3.491481338843133355E-15 ) ) ;
#618=EDGE_LOOP ( 'NONE', ( #5048, #5006, #2179, #2034 ) ) ;
#621=FACE_OUTER_BOUND ( 'NONE', #3054, .T. ) ;
#631=FACE_OUTER_BOUND ( 'NONE', #5917, .T. ) ;
#635=VERTEX_POINT ( 'NONE', #347 ) ;
#644=CIRCLE ( 'NONE', #5781, 0.8509999999999999787 ) ;
#655=SHAPE_DEFINITION_REPRESENTATION ( #1105, #951 ) ;
#659=DIRECTION ( 'NONE',  ( -1.000000000000000000, -0.000000000000000000, -0.000000000000000000 ) ) ;
#662=ORIENTED_EDGE ( 'NONE', *, *, #2796, .F. ) ;
#664=ORIENTED_EDGE ( 'NONE', *, *, #5133, .F. ) ;
#665=CARTESIAN_POINT ( 'NONE',  ( 1.849560077140141257, -0.7556913915602415655, -0.5150000000000000133 ) ) ;
#667=DIRECTION ( 'NONE',  ( 1.000000000000000000, 0.000000000000000000, 0.000000000000000000 ) ) ;
#670=FACE_OUTER_BOUND ( 'NONE', #1139, .T. ) ;
#672=EDGE_LOOP ( 'NONE', ( #2871, #913, #5493, #5863 ) ) ;
#679=ORIENTED_EDGE ( 'NONE', *, *, #761, .F. ) ;
#687=DIRECTION ( 'NONE',  ( -1.000000000000000000, -0.000000000000000000, -0.000000000000000000 ) ) ;
#691=CARTESIAN_POINT ( 'NONE',  ( 2.740000000000000213, -0.5150000000000034550, 0.9838866223909985553 ) ) ;
#692=FACE_OUTER_BOUND ( 'NONE', #2283, .T. ) ;
#703=CIRCLE ( 'NONE', #318, 7.864440107515624945 ) ;
#704=VECTOR ( 'NONE', #489, 1000.000000000000341 ) ;
#729=DIRECTION ( 'NONE',  ( -1.000000000000000000, -0.000000000000000000, -0.000000000000000000 ) ) ;
#744=ORIENTED_EDGE ( 'NONE', *, *, #1156, .T. ) ;
#746=CARTESIAN_POINT ( 'NONE',  ( 0.9586399445693771781, -0.5149999999999964606, -0.8293189044373090457 ) ) ;
#751=EDGE_CURVE ( 'NONE', #4020, #342, #703, .T. ) ;
#752=ORIENTED_EDGE ( 'NONE', *, *, #5216, .F. ) ;
#760=CARTESIAN_POINT ( 'NONE',  ( 2.740000000000000213, 0.9838866223910001096, 0.5149999999999999023 ) ) ;
#761=EDGE_CURVE ( 'NONE', #3012, #1071, #546, .T. ) ;
#766=AXIS2_PLACEMENT_3D ( 'NONE', #2403, #4266, #2375 ) ;
#767=DIRECTION ( 'NONE',  ( 0.000000000000000000, 0.000000000000000000, 1.000000000000000000 ) ) ;
#770=CARTESIAN_POINT ( 'NONE',  ( 19.70000000000000284, 3.061616997868383141E-16, -2.500000000000000000 ) ) ;
#773=ORIENTED_EDGE ( 'NONE', *, *, #751, .T. ) ;
#777=VECTOR ( 'NONE', #5468, 1000.000000000000000 ) ;
#779=UNCERTAINTY_MEASURE_WITH_UNIT (LENGTH_MEASURE( 1.000000000000000082E-05 ), #1753, 'distance_accuracy_value', 'NONE');
#783=FILL_AREA_STYLE_COLOUR ( '', #132 ) ;
#785=CARTESIAN_POINT ( 'NONE',  ( 2.740000000000000213, 0.6774776749089228556, 0.5149999999999997913 ) ) ;
#787=CIRCLE ( 'NONE', #2331, 0.2000000000000000944 ) ;
#800=ADVANCED_FACE ( 'NONE', ( #4623 ), #374, .T. ) ;
#802=EDGE_LOOP ( 'NONE', ( #5147, #2545, #5941, #1768 ) ) ;
#805=VERTEX_POINT ( 'NONE', #4561 ) ;
#828=ADVANCED_FACE ( 'NONE', ( #2247 ), #4194, .F. ) ;
#834=ORIENTED_EDGE ( 'NONE', *, *, #3551, .F. ) ;
#837=AXIS2_PLACEMENT_3D ( 'NONE', #3251, #4553, #3698 ) ;
#839=CIRCLE ( 'NONE', #5777, 7.983406227920510467 ) ;
#843=FACE_OUTER_BOUND ( 'NONE', #2021, .T. ) ;
#850=CARTESIAN_POINT ( 'NONE',  ( -25.39999999999996305, 0.000000000000000000, 0.000000000000000000 ) ) ;
#857=CARTESIAN_POINT ( 'NONE',  ( -996.9834933385058093, 0.000000000000000000, 0.000000000000000000 ) ) ;
#875=VECTOR ( 'NONE', #5916, 1000.000000000000114 ) ;
#887=AXIS2_PLACEMENT_3D ( 'NONE', #3023, #3358, #3863 ) ;
#907=EDGE_CURVE ( 'NONE', #1750, #1825, #4990, .T. ) ;
#913=ORIENTED_EDGE ( 'NONE', *, *, #3587, .F. ) ;
#925=LINE ( 'NONE', #2779, #2328 ) ;
#931=DIRECTION ( 'NONE',  ( 0.000000000000000000, 0.000000000000000000, 1.000000000000000000 ) ) ;
#938=EDGE_CURVE ( 'NONE', #3605, #1770, #69, .T. ) ;
#944=ORIENTED_EDGE ( 'NONE', *, *, #1714, .F. ) ;
#950=CARTESIAN_POINT ( 'NONE',  ( 0.3226060873438401089, 2.189154565102731098, 0.5149999999999992362 ) ) ;
#951=SHAPE_REPRESENTATION ( 'pan head cross recess screw_iso_ISO 7045 - M5 x 16 - Z - 16N', ( #5080 ), #5845 ) ;
#954=DIRECTION ( 'NONE',  ( 0.000000000000000000, -2.105246936865057790E-16, 1.000000000000000000 ) ) ;
#965=CIRCLE ( 'NONE', #403, 4.750000000000000000 ) ;
#975=AXIS2_PLACEMENT_3D ( 'NONE', #4360, #1103, #3898 ) ;
#982=ADVANCED_FACE ( 'NONE', ( #4195 ), #5945, .F. ) ;
#990=ORIENTED_EDGE ( 'NONE', *, *, #3538, .T. ) ;
#999=ORIENTED_EDGE ( 'NONE', *, *, #5216, .T. ) ;
#1005=DIRECTION ( 'NONE',  ( -1.000000000000000000, -0.000000000000000000, -0.000000000000000000 ) ) ;
#1012=ADVANCED_FACE ( 'NONE', ( #2600 ), #5375, .T. ) ;
#1021=CARTESIAN_POINT ( 'NONE',  ( 0.9586399445693629673, -0.5150000000000024558, 0.8293189044373063812 ) ) ;
#1030=CARTESIAN_POINT ( 'NONE',  ( 2.740000000000000213, 0.000000000000000000, 0.000000000000000000 ) ) ;
#1038=DIRECTION ( 'NONE',  ( 0.000000000000000000, 0.000000000000000000, -1.000000000000000000 ) ) ;
#1040=CARTESIAN_POINT ( 'NONE',  ( 0.000000000000000000, -0.5150000000000080069, 2.349999999999998312 ) ) ;
#1053=EDGE_CURVE ( 'NONE', #1098, #3585, #3242, .T. ) ;
#1058=CARTESIAN_POINT ( 'NONE',  ( 0.000000000000000000, 0.5149999999999917977, 2.350000000000000089 ) ) ;
#1060=ORIENTED_EDGE ( 'NONE', *, *, #1419, .T. ) ;
#1061=VECTOR ( 'NONE', #3800, 1000.000000000000000 ) ;
#1071=VERTEX_POINT ( 'NONE', #3002 ) ;
#1072=VECTOR ( 'NONE', #4368, 1000.000000000000114 ) ;
#1080=CARTESIAN_POINT ( 'NONE',  ( 8.000000000000000000, -4.837354856632045452E-15, 0.000000000000000000 ) ) ;
#1090=ORIENTED_EDGE ( 'NONE', *, *, #1641, .F. ) ;
#1098=VERTEX_POINT ( 'NONE', #3095 ) ;
#1103=DIRECTION ( 'NONE',  ( 1.007709689656716938E-16, 1.153406566473941260E-16, -1.000000000000000000 ) ) ;
#1105=PRODUCT_DEFINITION_SHAPE ( 'NONE', 'NONE',  #2280 ) ;
#1106=PRODUCT_CONTEXT ( 'NONE', #5950, 'mechanical' ) ;
#1109=LINE ( 'NONE', #691, #3490 ) ;
#1110=CARTESIAN_POINT ( 'NONE',  ( 3.900000000000000799, 3.306546357697853733E-16, -2.700000000000000178 ) ) ;
#1124=ORIENTED_EDGE ( 'NONE', *, *, #3551, .T. ) ;
#1131=LINE ( 'NONE', #1040, #3987 ) ;
#1139=EDGE_LOOP ( 'NONE', ( #5706, #5444, #4453, #2714 ) ) ;
#1148=EDGE_CURVE ( 'NONE', #805, #2324, #239, .T. ) ;
#1151=EDGE_CURVE ( 'NONE', #2598, #2324, #5821, .T. ) ;
#1154=DIRECTION ( 'NONE',  ( 0.000000000000000000, 1.000000000000000000, 1.153406566473941260E-16 ) ) ;
#1156=EDGE_CURVE ( 'NONE', #3272, #1472, #2207, .T. ) ;
#1170=FACE_OUTER_BOUND ( 'NONE', #618, .T. ) ;
#1171=ORIENTED_EDGE ( 'NONE', *, *, #4399, .T. ) ;
#1184=CARTESIAN_POINT ( 'NONE',  ( 0.000000000000000000, 2.350000000000000089, -0.5150000000000000133 ) ) ;
#1195=ADVANCED_FACE ( 'NONE', ( #5555 ), #3607, .T. ) ;
#1208=ORIENTED_EDGE ( 'NONE', *, *, #1360, .F. ) ;
#1229=DIRECTION ( 'NONE',  ( -1.000000000000000000, -0.000000000000000000, -0.000000000000000000 ) ) ;
#1237=SURFACE_STYLE_USAGE ( .BOTH. , #1355 ) ;
#1242=EDGE_CURVE ( 'NONE', #4005, #1098, #4418, .T. ) ;
#1259=( GEOMETRIC_REPRESENTATION_CONTEXT ( 3 ) GLOBAL_UNCERTAINTY_ASSIGNED_CONTEXT ( ( #2455 ) ) GLOBAL_UNIT_ASSIGNED_CONTEXT ( ( #2489, #5176, #194 ) ) REPRESENTATION_CONTEXT ( 'NONE', 'WORKASPACE' ) );
#1274=ADVANCED_FACE ( 'NONE', ( #454 ), #4524, .F. ) ;
#1279=ADVANCED_FACE ( 'NONE', ( #2668 ), #4230, .F. ) ;
#1294=CARTESIAN_POINT ( 'NONE',  ( 7.345657149124340535, -9.419606183588304946E-15, 1.312408941150045472 ) ) ;
#1302=ORIENTED_EDGE ( 'NONE', *, *, #1688, .F. ) ;
#1306=EDGE_CURVE ( 'NONE', #1563, #4461, #5399, .T. ) ;
#1308=EDGE_CURVE ( 'NONE', #5283, #805, #3833, .T. ) ;
#1312=CARTESIAN_POINT ( 'NONE',  ( 0.000000000000000000, -0.5149999999999909095, -2.350000000000000977 ) ) ;
#1313=ORIENTED_EDGE ( 'NONE', *, *, #5182, .F. ) ;
#1315=CARTESIAN_POINT ( 'NONE',  ( 2.740000000000000213, -0.6774776749089230776, 0.5149999999999995692 ) ) ;
#1324=CARTESIAN_POINT ( 'NONE',  ( 0.06760930072668806801, -4.837354856632045452E-15, 0.000000000000000000 ) ) ;
#1326=CARTESIAN_POINT ( 'NONE',  ( 8.000000000000000000, -0.5149999999999999023, -1.857513327677604022E-15 ) ) ;
#1330=AXIS2_PLACEMENT_3D ( 'NONE', #3944, #3554, #5404 ) ;
#1334=VERTEX_POINT ( 'NONE', #36 ) ;
#1336=CIRCLE ( 'NONE', #2114, 7.864440107515430434 ) ;
#1338=ORIENTED_EDGE ( 'NONE', *, *, #3975, .F. ) ;
#1353=CIRCLE ( 'NONE', #4747, 4.556291390728477886 ) ;
#1355=SURFACE_SIDE_STYLE ('',( #5644 ) ) ;
#1360=EDGE_CURVE ( 'NONE', #1588, #1770, #5159, .T. ) ;
#1372=ORIENTED_EDGE ( 'NONE', *, *, #3013, .F. ) ;
#1373=AXIS2_PLACEMENT_3D ( 'NONE', #3790, #1996, #2915 ) ;
#1376=DIRECTION ( 'NONE',  ( -1.000000000000000000, -0.000000000000000000, -0.000000000000000000 ) ) ;
#1379=DIRECTION ( 'NONE',  ( 0.000000000000000000, 0.000000000000000000, 1.000000000000000000 ) ) ;
#1385=LINE ( 'NONE', #5099, #5546 ) ;
#1391=CARTESIAN_POINT ( 'NONE',  ( 1.424271237134740131, 0.000000000000000000, 0.000000000000000000 ) ) ;
#1395=DIRECTION ( 'NONE',  ( 0.4461977533473793778, -2.936240938438015166E-15, 0.8949343913984707521 ) ) ;
#1403=VERTEX_POINT ( 'NONE', #4704 ) ;
#1404=ORIENTED_EDGE ( 'NONE', *, *, #565, .F. ) ;
#1405=AXIS2_PLACEMENT_3D ( 'NONE', #101, #1936, #2917 ) ;
#1407=PLANE ( 'NONE',  #766 ) ;
#1409=CARTESIAN_POINT ( 'NONE',  ( 2.740000000000000213, 0.9838866223910003317, 0.5149999999999999023 ) ) ;
#1412=CIRCLE ( 'NONE', #2382, 0.8509999999999999787 ) ;
#1416=CIRCLE ( 'NONE', #4234, 2.500000000000000000 ) ;
#1419=EDGE_CURVE ( 'NONE', #4278, #199, #2544, .T. ) ;
#1431=CARTESIAN_POINT ( 'NONE',  ( 3.700000000000000178, 0.000000000000000000, 0.000000000000000000 ) ) ;
#1434=SPHERICAL_SURFACE ( 'NONE', #3606, 8.000000000000000000 ) ;
#1437=AXIS2_PLACEMENT_3D ( 'NONE', #3828, #3856, #1154 ) ;
#1439=CARTESIAN_POINT ( 'NONE',  ( 2.740000000000000213, 0.5150000000000024558, -0.6774776749089207462 ) ) ;
#1449=EDGE_CURVE ( 'NONE', #2799, #1334, #1412, .T. ) ;
#1456=CARTESIAN_POINT ( 'NONE',  ( 2.740000000000000213, 0.000000000000000000, 0.000000000000000000 ) ) ;
#1462=AXIS2_PLACEMENT_3D ( 'NONE', #2561, #4973, #4484 ) ;
#1465=EDGE_CURVE ( 'NONE', #5831, #1830, #5114, .T. ) ;
#1472=VERTEX_POINT ( 'NONE', #5278 ) ;
#1480=VERTEX_POINT ( 'NONE', #2537 ) ;
#1485=AXIS2_PLACEMENT_3D ( 'NONE', #2148, #729, #275 ) ;
#1492=CLOSED_SHELL ( 'NONE', ( #3520, #828, #4166, #800, #1012, #5772, #4546, #4729, #1195, #2843, #1970, #4319, #2376, #1795, #2420, #244, #277, #4691, #5466, #5573, #5676, #3866, #3096, #3469, #4619, #349, #359, #1907, #5471, #1274, #5504, #1279, #5853, #982 ) ) ;
#1499=FACE_OUTER_BOUND ( 'NONE', #4988, .T. ) ;
#1505=CARTESIAN_POINT ( 'NONE',  ( 1.849560077140107284, 0.5150000000000026779, -0.7556913915602427867 ) ) ;
#1508=LINE ( 'NONE', #3365, #3512 ) ;
#1513=AXIS2_PLACEMENT_3D ( 'NONE', #3028, #3450, #1629 ) ;
#1514=FACE_OUTER_BOUND ( 'NONE', #99, .T. ) ;
#1517=B_SPLINE_CURVE_WITH_KNOTS ( 'NONE', 3,
 ( #4916, #746, #2993, #4849 ),
 .UNSPECIFIED., .F., .F.,
 ( 4, 4 ),
 ( 0.001586480563516617188, 0.004268227385920363680 ),
 .UNSPECIFIED. ) ;
#1533=CARTESIAN_POINT ( 'NONE',  ( 2.740000000000000213, 0.5149999999999976819, 0.6774776749089244099 ) ) ;
#1562=DIRECTION ( 'NONE',  ( 0.000000000000000000, 0.000000000000000000, 1.000000000000000000 ) ) ;
#1563=VERTEX_POINT ( 'NONE', #3901 ) ;
#1572=LINE ( 'NONE', #2940, #5440 ) ;
#1587=DIRECTION ( 'NONE',  ( 0.000000000000000000, 0.000000000000000000, 1.000000000000000000 ) ) ;
#1588=VERTEX_POINT ( 'NONE', #5784 ) ;
#1595=CARTESIAN_POINT ( 'NONE',  ( 7.345657149124338758, 1.312408941150044583, 0.000000000000000000 ) ) ;
#1599=CARTESIAN_POINT ( 'NONE',  ( 3.700000000000000178, 0.000000000000000000, 0.000000000000000000 ) ) ;
#1602=EDGE_LOOP ( 'NONE', ( #662, #1338, #4474, #4542, #4506 ) ) ;
#1604=B_SPLINE_CURVE_WITH_KNOTS ( 'NONE', 3,
 ( #257, #2095, #1021, #2742 ),
 .UNSPECIFIED., .F., .F.,
 ( 4, 4 ),
 ( 0.004656695506220393486, 0.007337072593346777132 ),
 .UNSPECIFIED. ) ;
#1615=EDGE_CURVE ( 'NONE', #4278, #5342, #644, .T. ) ;
#1617=EDGE_CURVE ( 'NONE', #805, #171, #1517, .T. ) ;
#1619=ORIENTED_EDGE ( 'NONE', *, *, #491, .F. ) ;
#1622=ORIENTED_EDGE ( 'NONE', *, *, #2648, .F. ) ;
#1629=DIRECTION ( 'NONE',  ( -0.8949343913984706411, 0.4461977533473793223, 0.000000000000000000 ) ) ;
#1634=ORIENTED_EDGE ( 'NONE', *, *, #2645, .T. ) ;
#1636=ORIENTED_EDGE ( 'NONE', *, *, #491, .T. ) ;
#1641=EDGE_CURVE ( 'NONE', #553, #3979, #1416, .T. ) ;
#1649=FACE_OUTER_BOUND ( 'NONE', #3772, .T. ) ;
#1651=DIRECTION ( 'NONE',  ( 0.000000000000000000, -3.612465276695121047E-15, 1.000000000000000000 ) ) ;
#1656=CARTESIAN_POINT ( 'NONE',  ( 0.3226060873438262311, -0.5149999999999915756, -2.189154565102686245 ) ) ;
#1662=AXIS2_PLACEMENT_3D ( 'NONE', #2567, #2473, #179 ) ;
#1665=CARTESIAN_POINT ( 'NONE',  ( 3.700000000000000178, 2.500000000000000000, 0.000000000000000000 ) ) ;
#1667=ORIENTED_EDGE ( 'NONE', *, *, #761, .T. ) ;
#1674=B_SPLINE_CURVE_WITH_KNOTS ( 'NONE', 3,
 ( #143, #5178, #5541, #4268 ),
 .UNSPECIFIED., .F., .F.,
 ( 4, 4 ),
 ( 0.001586480565025038831, 0.004268227387428736967 ),
 .UNSPECIFIED. ) ;
#1688=EDGE_CURVE ( 'NONE', #5283, #3078, #1336, .T. ) ;
#1689=ORIENTED_EDGE ( 'NONE', *, *, #3248, .F. ) ;
#1698=DIRECTION ( 'NONE',  ( 0.000000000000000000, 1.224646799147353207E-16, -1.000000000000000000 ) ) ;
#1714=EDGE_CURVE ( 'NONE', #3630, #1472, #606, .T. ) ;
#1716=CARTESIAN_POINT ( 'NONE',  ( 1.794155980045911036, 0.000000000000000000, 0.000000000000000000 ) ) ;
#1729=EDGE_CURVE ( 'NONE', #1825, #1750, #2196, .T. ) ;
#1740=DIRECTION ( 'NONE',  ( 1.007709689656716938E-16, 1.153406566473941260E-16, -1.000000000000000000 ) ) ;
#1741=VERTEX_POINT ( 'NONE', #337 ) ;
#1750=VERTEX_POINT ( 'NONE', #3569 ) ;
#1753=( LENGTH_UNIT ( ) NAMED_UNIT ( * ) SI_UNIT ( .MILLI., .METRE. ) );
#1755=CARTESIAN_POINT ( 'NONE',  ( -25.39999999999996305, 5.817072295949926440E-16, -4.749999999999999112 ) ) ;
#1759=FACE_OUTER_BOUND ( 'NONE', #3035, .T. ) ;
#1766=CIRCLE ( 'NONE', #4590, 8.000000000000000000 ) ;
#1768=ORIENTED_EDGE ( 'NONE', *, *, #1729, .F. ) ;
#1770=VERTEX_POINT ( 'NONE', #5871 ) ;
#1782=DIRECTION ( 'NONE',  ( -0.000000000000000000, 0.000000000000000000, 1.000000000000000000 ) ) ;
#1795=ADVANCED_FACE ( 'NONE', ( #3601 ), #4578, .T. ) ;
#1801=ORIENTED_EDGE ( 'NONE', *, *, #5050, .T. ) ;
#1806=CARTESIAN_POINT ( 'NONE',  ( 3.900000000000000799, 0.000000000000000000, 0.000000000000000000 ) ) ;
#1812=DIRECTION ( 'NONE',  ( -0.000000000000000000, 0.000000000000000000, 1.000000000000000000 ) ) ;
#1821=DIRECTION ( 'NONE',  ( -0.000000000000000000, 0.000000000000000000, 1.000000000000000000 ) ) ;
#1825=VERTEX_POINT ( 'NONE', #2318 ) ;
#1828=CARTESIAN_POINT ( 'NONE',  ( 0.000000000000000000, 2.350000000000000089, 0.5149999999999996803 ) ) ;
#1830=VERTEX_POINT ( 'NONE', #950 ) ;
#1831=ORIENTED_EDGE ( 'NONE', *, *, #1306, .T. ) ;
#1842=EDGE_CURVE ( 'NONE', #553, #1750, #4665, .T. ) ;
#1874=AXIS2_PLACEMENT_3D ( 'NONE', #3127, #1812, #4155 ) ;
#1879=ORIENTED_EDGE ( 'NONE', *, *, #5132, .T. ) ;
#1881=FACE_OUTER_BOUND ( 'NONE', #5376, .T. ) ;
#1884=ORIENTED_EDGE ( 'NONE', *, *, #3687, .F. ) ;
#1892=DIRECTION ( 'NONE',  ( -0.000000000000000000, 0.000000000000000000, -1.000000000000000000 ) ) ;
#1907=ADVANCED_FACE ( 'NONE', ( #4723 ), #1407, .F. ) ;
#1928=ORIENTED_EDGE ( 'NONE', *, *, #4724, .T. ) ;
#1936=DIRECTION ( 'NONE',  ( -1.000000000000000000, -0.000000000000000000, -0.000000000000000000 ) ) ;
#1938=VECTOR ( 'NONE', #4143, 1000.000000000000114 ) ;
#1939=DIRECTION ( 'NONE',  ( -1.000000000000000000, -0.000000000000000000, -0.000000000000000000 ) ) ;
#1940=EDGE_CURVE ( 'NONE', #1480, #5831, #5047, .T. ) ;
#1952=ORIENTED_EDGE ( 'NONE', *, *, #280, .F. ) ;
#1955=CARTESIAN_POINT ( 'NONE',  ( 0.9586399445693630783, 0.5150000000000030109, -0.8293189044373061591 ) ) ;
#1958=DIRECTION ( 'NONE',  ( -0.000000000000000000, 1.000000000000000000, 1.224646799147353207E-16 ) ) ;
#1967=DIRECTION ( 'NONE',  ( 0.000000000000000000, 0.000000000000000000, 1.000000000000000000 ) ) ;
#1970=ADVANCED_FACE ( 'NONE', ( #621 ), #2466, .T. ) ;
#1983=VERTEX_POINT ( 'NONE', #142 ) ;
#1986=DIRECTION ( 'NONE',  ( -1.000000000000000000, -0.000000000000000000, -0.000000000000000000 ) ) ;
#1987=DIRECTION ( 'NONE',  ( 1.000000000000000000, 0.000000000000000000, 0.000000000000000000 ) ) ;
#1996=DIRECTION ( 'NONE',  ( -1.000000000000000000, -0.000000000000000000, -0.000000000000000000 ) ) ;
#2016=FACE_OUTER_BOUND ( 'NONE', #4826, .T. ) ;
#2017=DIRECTION ( 'NONE',  ( 0.000000000000000000, 1.000000000000000000, 0.000000000000000000 ) ) ;
#2019=EDGE_CURVE ( 'NONE', #3083, #342, #3097, .T. ) ;
#2021=EDGE_LOOP ( 'NONE', ( #3936, #1667, #5852, #3510 ) ) ;
#2025=CARTESIAN_POINT ( 'NONE',  ( 2.740000000000000213, -0.6774776749089226335, -0.5150000000000000133 ) ) ;
#2028=VERTEX_POINT ( 'NONE', #4876 ) ;
#2029=CIRCLE ( 'NONE', #3584, 4.749999999999999112 ) ;
#2034=ORIENTED_EDGE ( 'NONE', *, *, #2195, .F. ) ;
#2035=AXIS2_PLACEMENT_3D ( 'NONE', #4550, #2632, #393 ) ;
#2040=AXIS2_PLACEMENT_3D ( 'NONE', #5893, #1740, #4045 ) ;
#2046=AXIS2_PLACEMENT_3D ( 'NONE', #2203, #300, #4052 ) ;
#2051=CARTESIAN_POINT ( 'NONE',  ( 1.849560077140140812, 0.5149999999999973488, 0.7556913915602433418 ) ) ;
#2059=VERTEX_POINT ( 'NONE', #4419 ) ;
#2074=ORIENTED_EDGE ( 'NONE', *, *, #1465, .T. ) ;
#2083=DIRECTION ( 'NONE',  ( 0.000000000000000000, 0.000000000000000000, 1.000000000000000000 ) ) ;
#2084=CARTESIAN_POINT ( 'NONE',  ( 0.000000000000000000, 0.5150000000000083400, -2.349999999999997424 ) ) ;
#2087=ORIENTED_EDGE ( 'NONE', *, *, #4093, .F. ) ;
#2093=ORIENTED_EDGE ( 'NONE', *, *, #2645, .F. ) ;
#2095=CARTESIAN_POINT ( 'NONE',  ( 1.849560077140107950, -0.5150000000000023448, 0.7556913915602430087 ) ) ;
#2101=DIRECTION ( 'NONE',  ( 0.000000000000000000, 0.000000000000000000, 1.000000000000000000 ) ) ;
#2107=CARTESIAN_POINT ( 'NONE',  ( 2.740000000000000213, 0.000000000000000000, 0.000000000000000000 ) ) ;
#2111=FACE_BOUND ( 'NONE', #3656, .T. ) ;
#2112=LINE ( 'NONE', #3933, #5934 ) ;
#2113=ORIENTED_EDGE ( 'NONE', *, *, #3287, .T. ) ;
#2114=AXIS2_PLACEMENT_3D ( 'NONE', #1294, #2201, #2268 ) ;
#2120=EDGE_CURVE ( 'NONE', #2598, #4174, #2215, .T. ) ;
#2130=ORIENTED_EDGE ( 'NONE', *, *, #5761, .T. ) ;
#2131=CARTESIAN_POINT ( 'NONE',  ( 3.699999999999998401, 0.000000000000000000, 0.000000000000000000 ) ) ;
#2144=ORIENTED_EDGE ( 'NONE', *, *, #4737, .F. ) ;
#2148=CARTESIAN_POINT ( 'NONE',  ( -25.39999999999996305, 0.000000000000000000, 0.000000000000000000 ) ) ;
#2152=CARTESIAN_POINT ( 'NONE',  ( -25.39999999999996305, 0.000000000000000000, 4.749999999999999112 ) ) ;
#2157=CARTESIAN_POINT ( 'NONE',  ( 2.740000000000000213, -0.6774776749089226335, -0.5150000000000000133 ) ) ;
#2160=EDGE_CURVE ( 'NONE', #2555, #635, #3077, .T. ) ;
#2166=ORIENTED_EDGE ( 'NONE', *, *, #4514, .F. ) ;
#2174=DIRECTION ( 'NONE',  ( 0.000000000000000000, 0.000000000000000000, 1.000000000000000000 ) ) ;
#2176=CARTESIAN_POINT ( 'NONE',  ( 0.06760930072668894231, 0.9010842325122832008, -0.5150000000000000133 ) ) ;
#2179=ORIENTED_EDGE ( 'NONE', *, *, #2796, .T. ) ;
#2181=CARTESIAN_POINT ( 'NONE',  ( 0.9586399445693771781, -0.8293189044373066032, -0.5150000000000000133 ) ) ;
#2184=CARTESIAN_POINT ( 'NONE',  ( 2.740000000000000213, 0.9838866223910001096, -0.5150000000000001243 ) ) ;
#2190=ORIENTED_EDGE ( 'NONE', *, *, #5483, .T. ) ;
#2193=DIRECTION ( 'NONE',  ( 0.000000000000000000, 0.000000000000000000, 1.000000000000000000 ) ) ;
#2195=EDGE_CURVE ( 'NONE', #5283, #1741, #3175, .T. ) ;
#2196=CIRCLE ( 'NONE', #4926, 2.500000000000000000 ) ;
#2197=VERTEX_POINT ( 'NONE', #3108 ) ;
#2201=DIRECTION ( 'NONE',  ( 0.4461977533474923430, 3.124646727056501017E-15, -0.8949343913984144638 ) ) ;
#2203=CARTESIAN_POINT ( 'NONE',  ( -25.39999999999996305, 0.000000000000000000, 0.000000000000000000 ) ) ;
#2204=DIRECTION ( 'NONE',  ( 0.000000000000000000, 0.000000000000000000, 1.000000000000000000 ) ) ;
#2206=PRESENTATION_STYLE_ASSIGNMENT (( #1237 ) ) ;
#2207=LINE ( 'NONE', #1755, #2453 ) ;
#2210=ORIENTED_EDGE ( 'NONE', *, *, #751, .F. ) ;
#2211=DIRECTION ( 'NONE',  ( 0.000000000000000000, 0.000000000000000000, 1.000000000000000000 ) ) ;
#2215=CIRCLE ( 'NONE', #5605, 0.8509999999999999787 ) ;
#2231=CARTESIAN_POINT ( 'NONE',  ( 0.06760930072668813740, -0.5150000000000026779, 0.9010842325122891960 ) ) ;
#2238=AXIS2_PLACEMENT_3D ( 'NONE', #857, #4569, #3654 ) ;
#2247=FACE_OUTER_BOUND ( 'NONE', #2374, .T. ) ;
#2252=CIRCLE ( 'NONE', #5823, 1.037871761867652065 ) ;
#2260=CARTESIAN_POINT ( 'NONE',  ( 3.900000000000000799, 0.000000000000000000, 0.000000000000000000 ) ) ;
#2261=DIRECTION ( 'NONE',  ( -1.000000000000000000, -0.000000000000000000, -0.000000000000000000 ) ) ;
#2262=ORIENTED_EDGE ( 'NONE', *, *, #135, .F. ) ;
#2264=VERTEX_POINT ( 'NONE', #4689 ) ;
#2268=DIRECTION ( 'NONE',  ( -0.8949343913984144638, 0.000000000000000000, -0.4461977533474923430 ) ) ;
#2275=ORIENTED_EDGE ( 'NONE', *, *, #1449, .T. ) ;
#2277=DIRECTION ( 'NONE',  ( 0.000000000000000000, -1.224646799147352714E-16, 1.000000000000000000 ) ) ;
#2280=PRODUCT_DEFINITION ( 'UNKNOWN', '', #432, #4919 ) ;
#2283=EDGE_LOOP ( 'NONE', ( #5331, #1622, #1619, #4193 ) ) ;
#2286=DIRECTION ( 'NONE',  ( 0.000000000000000000, 3.656775105596099119E-15, -1.000000000000000000 ) ) ;
#2288=CARTESIAN_POINT ( 'NONE',  ( 2.740000000000000213, 0.5149999999999976819, 0.6774776749089244099 ) ) ;
#2298=ORIENTED_EDGE ( 'NONE', *, *, #5438, .F. ) ;
#2300=CARTESIAN_POINT ( 'NONE',  ( 2.740000000000000213, 0.000000000000000000, 0.000000000000000000 ) ) ;
#2316=EDGE_CURVE ( 'NONE', #1588, #2799, #4170, .T. ) ;
#2318=CARTESIAN_POINT ( 'NONE',  ( 3.900000000000000799, 3.061616997868383141E-16, -2.500000000000000000 ) ) ;
#2324=VERTEX_POINT ( 'NONE', #5529 ) ;
#2328=VECTOR ( 'NONE', #4238, 1000.000000000000000 ) ;
#2329=ORIENTED_EDGE ( 'NONE', *, *, #3538, .F. ) ;
#2331=AXIS2_PLACEMENT_3D ( 'NONE', #1110, #1958, #3391 ) ;
#2332=AXIS2_PLACEMENT_3D ( 'NONE', #3388, #3029, #1987 ) ;
#2334=ORIENTED_EDGE ( 'NONE', *, *, #4810, .F. ) ;
#2355=STYLED_ITEM ( 'NONE', ( #2206 ), #4058 ) ;
#2359=AXIS2_PLACEMENT_3D ( 'NONE', #3783, #3845, #5130 ) ;
#2369=DIRECTION ( 'NONE',  ( 0.000000000000000000, 0.000000000000000000, 1.000000000000000000 ) ) ;
#2374=EDGE_LOOP ( 'NONE', ( #2262, #5170, #4713, #2334 ) ) ;
#2375=DIRECTION ( 'NONE',  ( -0.8949343913984706411, -1.557891129246106096E-15, 0.4461977533473793223 ) ) ;
#2376=ADVANCED_FACE ( 'NONE', ( #2432 ), #4868, .T. ) ;
#2378=CIRCLE ( 'NONE', #4716, 0.8509999999999999787 ) ;
#2382=AXIS2_PLACEMENT_3D ( 'NONE', #149, #1986, #931 ) ;
#2393=DIRECTION ( 'NONE',  ( 0.000000000000000000, 0.000000000000000000, 1.000000000000000000 ) ) ;
#2402=ORIENTED_EDGE ( 'NONE', *, *, #4399, .F. ) ;
#2403=CARTESIAN_POINT ( 'NONE',  ( 2.740000000000000213, -0.5150000000000034550, 0.9838866223909985553 ) ) ;
#2417=CARTESIAN_POINT ( 'NONE',  ( 0.06760930072668894231, 0.9010842325122760954, 0.5149999999999993472 ) ) ;
#2420=ADVANCED_FACE ( 'NONE', ( #670 ), #5260, .T. ) ;
#2424=DIRECTION ( 'NONE',  ( 0.000000000000000000, 0.000000000000000000, 1.000000000000000000 ) ) ;
#2427=AXIS2_PLACEMENT_3D ( 'NONE', #3896, #4358, #2101 ) ;
#2431=VECTOR ( 'NONE', #5812, 1000.000000000000000 ) ;
#2432=FACE_OUTER_BOUND ( 'NONE', #1602, .T. ) ;
#2439=CARTESIAN_POINT ( 'NONE',  ( 8.000000000000000000, -0.5149999999999999023, -1.857513327677604022E-15 ) ) ;
#2453=VECTOR ( 'NONE', #4032, 1000.000000000000000 ) ;
#2455=UNCERTAINTY_MEASURE_WITH_UNIT (LENGTH_MEASURE( 1.000000000000000082E-05 ), #2489, 'distance_accuracy_value', 'NONE');
#2460=EDGE_CURVE ( 'NONE', #1098, #140, #1353, .T. ) ;
#2466=PLANE ( 'NONE',  #1437 ) ;
#2473=DIRECTION ( 'NONE',  ( -0.000000000000000000, 0.000000000000000000, 1.000000000000000000 ) ) ;
#2475=DIRECTION ( 'NONE',  ( -1.000000000000000000, -0.000000000000000000, -0.000000000000000000 ) ) ;
#2476=DIRECTION ( 'NONE',  ( 0.4461977533473793778, 0.8949343913984707521, -1.884057886186824742E-16 ) ) ;
#2485=DIRECTION ( 'NONE',  ( 1.000000000000000000, 0.000000000000000000, 0.000000000000000000 ) ) ;
#2489=( LENGTH_UNIT ( ) NAMED_UNIT ( * ) SI_UNIT ( .MILLI., .METRE. ) );
#2501=DIRECTION ( 'NONE',  ( 1.007709689656716815E-16, 1.000000000000000000, 3.606821995490527259E-15 ) ) ;
#2507=CARTESIAN_POINT ( 'NONE',  ( 8.000000000000000000, -4.837354856632045452E-15, 0.000000000000000000 ) ) ;
#2510=AXIS2_PLACEMENT_3D ( 'NONE', #5120, #2716, #3291 ) ;
#2514=AXIS2_PLACEMENT_3D ( 'NONE', #29, #4725, #1038 ) ;
#2520=DIRECTION ( 'NONE',  ( 0.000000000000000000, -1.000000000000000000, -3.491481338843133355E-15 ) ) ;
#2524=VECTOR ( 'NONE', #4486, 1000.000000000000341 ) ;
#2537=CARTESIAN_POINT ( 'NONE',  ( 0.3226060873438401089, 2.189154565102731098, -0.5150000000000000133 ) ) ;
#2539=DIRECTION ( 'NONE',  ( 0.000000000000000000, 0.000000000000000000, 1.000000000000000000 ) ) ;
#2541=DIRECTION ( 'NONE',  ( 0.8949343913984143528, 0.4461977533474921764, 1.416481476476136321E-16 ) ) ;
#2544=B_SPLINE_CURVE_WITH_KNOTS ( 'NONE', 3,
 ( #1439, #1505, #1955, #3301 ),
 .UNSPECIFIED., .F., .F.,
 ( 4, 4 ),
 ( 0.004656695506220393486, 0.007337072593346776264 ),
 .UNSPECIFIED. ) ;
#2545=ORIENTED_EDGE ( 'NONE', *, *, #2831, .F. ) ;
#2555=VERTEX_POINT ( 'NONE', #760 ) ;
#2556=DIRECTION ( 'NONE',  ( 0.000000000000000000, -3.606821995490527259E-15, 1.000000000000000000 ) ) ;
#2561=CARTESIAN_POINT ( 'NONE',  ( 1.794155980045909482, 0.000000000000000000, 0.000000000000000000 ) ) ;
#2567=CARTESIAN_POINT ( 'NONE',  ( 8.000000000000000000, -4.837354856632045452E-15, -0.5150000000000000133 ) ) ;
#2571=PLANE ( 'NONE',  #3695 ) ;
#2572=ORIENTED_EDGE ( 'NONE', *, *, #1156, .F. ) ;
#2576=EDGE_LOOP ( 'NONE', ( #4204, #1208, #5753, #2210 ) ) ;
#2578=EDGE_CURVE ( 'NONE', #1480, #635, #4505, .T. ) ;
#2590=ORIENTED_EDGE ( 'NONE', *, *, #3660, .T. ) ;
#2593=DIRECTION ( 'NONE',  ( -1.000000000000000000, -0.000000000000000000, -0.000000000000000000 ) ) ;
#2594=PLANE ( 'NONE',  #4655 ) ;
#2598=VERTEX_POINT ( 'NONE', #2157 ) ;
#2600=FACE_OUTER_BOUND ( 'NONE', #4017, .T. ) ;
#2615=DIRECTION ( 'NONE',  ( 0.000000000000000000, -2.105246936865057050E-16, -1.000000000000000000 ) ) ;
#2632=DIRECTION ( 'NONE',  ( 0.000000000000000000, -1.000000000000000000, 0.000000000000000000 ) ) ;
#2638=AXIS2_PLACEMENT_3D ( 'NONE', #850, #2701, #2211 ) ;
#2640=AXIS2_PLACEMENT_3D ( 'NONE', #1665, #3961, #1782 ) ;
#2645=EDGE_CURVE ( 'NONE', #3979, #1825, #4415, .T. ) ;
#2648=EDGE_CURVE ( 'NONE', #2799, #3083, #1604, .T. ) ;
#2663=DIRECTION ( 'NONE',  ( 0.000000000000000000, 0.000000000000000000, 1.000000000000000000 ) ) ;
#2668=FACE_OUTER_BOUND ( 'NONE', #3798, .T. ) ;
#2690=FACE_OUTER_BOUND ( 'NONE', #3594, .T. ) ;
#2691=CIRCLE ( 'NONE', #1330, 0.4499999999999985678 ) ;
#2701=DIRECTION ( 'NONE',  ( -1.000000000000000000, -0.000000000000000000, -0.000000000000000000 ) ) ;
#2708=ORIENTED_EDGE ( 'NONE', *, *, #2120, .F. ) ;
#2714=ORIENTED_EDGE ( 'NONE', *, *, #5738, .F. ) ;
#2716=DIRECTION ( 'NONE',  ( 0.000000000000000000, -1.000000000000000000, -3.491481338843133355E-15 ) ) ;
#2726=AXIS2_PLACEMENT_3D ( 'NONE', #302, #341, #2204 ) ;
#2728=TOROIDAL_SURFACE ( 'NONE', #113, 2.700000000000000178, 0.2000000000000000111 ) ;
#2729=CARTESIAN_POINT ( 'NONE',  ( 0.06760930072668894231, 0.9010842325122760954, 0.5149999999999993472 ) ) ;
#2733=AXIS2_PLACEMENT_3D ( 'NONE', #446, #2261, #2773 ) ;
#2742=CARTESIAN_POINT ( 'NONE',  ( 0.06760930072668813740, -0.5150000000000026779, 0.9010842325122891960 ) ) ;
#2746=FACE_OUTER_BOUND ( 'NONE', #3891, .T. ) ;
#2754=ORIENTED_EDGE ( 'NONE', *, *, #2864, .T. ) ;
#2760=ORIENTED_EDGE ( 'NONE', *, *, #4370, .F. ) ;
#2773=DIRECTION ( 'NONE',  ( 0.000000000000000000, -3.552713678800500929E-15, -1.000000000000000000 ) ) ;
#2776=VECTOR ( 'NONE', #63, 1000.000000000000000 ) ;
#2779=CARTESIAN_POINT ( 'NONE',  ( 2.740000000000000213, 0.5150000000000035660, -0.9838866223905657904 ) ) ;
#2781=CARTESIAN_POINT ( 'NONE',  ( 8.000000000000000000, -4.837354856632045452E-15, 0.000000000000000000 ) ) ;
#2788=VERTEX_POINT ( 'NONE', #4732 ) ;
#2790=CARTESIAN_POINT ( 'NONE',  ( 2.740000000000000213, 0.6774776749089226335, -0.5150000000000000133 ) ) ;
#2796=EDGE_CURVE ( 'NONE', #171, #1741, #1109, .T. ) ;
#2799=VERTEX_POINT ( 'NONE', #5721 ) ;
#2831=EDGE_CURVE ( 'NONE', #5067, #2028, #5054, .T. ) ;
#2832=AXIS2_PLACEMENT_3D ( 'NONE', #4501, #345, #2277 ) ;
#2839=LINE ( 'NONE', #1409, #222 ) ;
#2843=ADVANCED_FACE ( 'NONE', ( #4428 ), #2594, .T. ) ;
#2852=VERTEX_POINT ( 'NONE', #5814 ) ;
#2859=ORIENTED_EDGE ( 'NONE', *, *, #1151, .F. ) ;
#2863=CARTESIAN_POINT ( 'NONE',  ( -25.39999999999996305, 0.000000000000000000, 2.500000000000000000 ) ) ;
#2864=EDGE_CURVE ( 'NONE', #1472, #3630, #2029, .T. ) ;
#2871=ORIENTED_EDGE ( 'NONE', *, *, #5050, .F. ) ;
#2889=ORIENTED_EDGE ( 'NONE', *, *, #537, .T. ) ;
#2909=ORIENTED_EDGE ( 'NONE', *, *, #2120, .T. ) ;
#2915=DIRECTION ( 'NONE',  ( 0.000000000000000000, 0.000000000000000000, 1.000000000000000000 ) ) ;
#2917=DIRECTION ( 'NONE',  ( 0.000000000000000000, 0.000000000000000000, -1.000000000000000000 ) ) ;
#2918=AXIS2_PLACEMENT_3D ( 'NONE', #3033, #2501, #5816 ) ;
#2925=ORIENTED_EDGE ( 'NONE', *, *, #458, .F. ) ;
#2933=CARTESIAN_POINT ( 'NONE',  ( 3.700000000000000178, 0.000000000000000000, 2.700000000000000178 ) ) ;
#2940=CARTESIAN_POINT ( 'NONE',  ( 2.740000000000000213, 0.9838866223910003317, 0.5149999999999999023 ) ) ;
#2944=ORIENTED_EDGE ( 'NONE', *, *, #135, .T. ) ;
#2946=CARTESIAN_POINT ( 'NONE',  ( -996.9834933385058093, 0.000000000000000000, 0.000000000000000000 ) ) ;
#2993=CARTESIAN_POINT ( 'NONE',  ( 1.849560077140141701, -0.5149999999999969047, -0.7556913915602436749 ) ) ;
#2997=DIRECTION ( 'NONE',  ( 0.4461977533474923430, 3.124646727056501411E-15, -0.8949343913984144638 ) ) ;
#3002=CARTESIAN_POINT ( 'NONE',  ( 2.740000000000000213, 0.6774776749089226335, -0.5150000000000000133 ) ) ;
#3009=AXIS2_PLACEMENT_3D ( 'NONE', #3017, #5774, #2556 ) ;
#3012=VERTEX_POINT ( 'NONE', #2176 ) ;
#3013=EDGE_CURVE ( 'NONE', #2059, #3272, #965, .T. ) ;
#3014=ORIENTED_EDGE ( 'NONE', *, *, #496, .T. ) ;
#3017=CARTESIAN_POINT ( 'NONE',  ( 0.000000000000000000, -0.5149999999999909095, -2.349999999999999201 ) ) ;
#3019=DIRECTION ( 'NONE',  ( 1.007709689656716938E-16, 1.000000000000000000, 3.606821995490528048E-15 ) ) ;
#3023=CARTESIAN_POINT ( 'NONE',  ( 7.345657149124338758, 1.312408941150044583, 0.000000000000000000 ) ) ;
#3025=AXIS2_PLACEMENT_3D ( 'NONE', #73, #3757, #1967 ) ;
#3028=CARTESIAN_POINT ( 'NONE',  ( 7.345657149124971141, -1.312408941149200814, 2.762944903268657774E-16 ) ) ;
#3029=DIRECTION ( 'NONE',  ( -0.000000000000000000, 0.000000000000000000, 1.000000000000000000 ) ) ;
#3033=CARTESIAN_POINT ( 'NONE',  ( 0.000000000000000000, -0.5149999999999909095, -2.349999999999999201 ) ) ;
#3035=EDGE_LOOP ( 'NONE', ( #2298, #2708, #4601, #4778 ) ) ;
#3038=DIRECTION ( 'NONE',  ( -1.000000000000000000, -0.000000000000000000, -0.000000000000000000 ) ) ;
#3046=AXIS2_PLACEMENT_3D ( 'NONE', #4345, #3038, #186 ) ;
#3054=EDGE_LOOP ( 'NONE', ( #1879, #382, #3067, #4938 ) ) ;
#3058=DIRECTION ( 'NONE',  ( 0.000000000000000000, 0.000000000000000000, 1.000000000000000000 ) ) ;
#3067=ORIENTED_EDGE ( 'NONE', *, *, #5438, .T. ) ;
#3077=LINE ( 'NONE', #4040, #3759 ) ;
#3078=VERTEX_POINT ( 'NONE', #4548 ) ;
#3079=LINE ( 'NONE', #1828, #1938 ) ;
#3083=VERTEX_POINT ( 'NONE', #2231 ) ;
#3084=CARTESIAN_POINT ( 'NONE',  ( 19.70000000000000284, 0.000000000000000000, 0.000000000000000000 ) ) ;
#3089=DIRECTION ( 'NONE',  ( 0.000000000000000000, -2.664535259100375697E-15, -1.000000000000000000 ) ) ;
#3095=CARTESIAN_POINT ( 'NONE',  ( 1.424271237134740131, -4.556291390728484991, -5.579847667638274858E-16 ) ) ;
#3096=ADVANCED_FACE ( 'NONE', ( #4301 ), #505, .T. ) ;
#3097=CIRCLE ( 'NONE', #5324, 7.983406227920510467 ) ;
#3103=ORIENTED_EDGE ( 'NONE', *, *, #5903, .T. ) ;
#3108=CARTESIAN_POINT ( 'NONE',  ( 0.06760930072668799862, 0.5149999999999969047, 0.9010842325122926377 ) ) ;
#3111=DIRECTION ( 'NONE',  ( -1.000000000000000000, -0.000000000000000000, -0.000000000000000000 ) ) ;
#3112=CIRCLE ( 'NONE', #492, 0.8509999999999999787 ) ;
#3114=CARTESIAN_POINT ( 'NONE',  ( 3.016506661494197328, 8.581769150706125103E-33, -7.007546303702493782E-17 ) ) ;
#3115=CIRCLE ( 'NONE', #3302, 4.556291390728477886 ) ;
#3119=CONICAL_SURFACE ( 'NONE', #2238, 3077.683537175319998, 1.256637061435923686 ) ;
#3127=CARTESIAN_POINT ( 'NONE',  ( 0.000000000000000000, 2.349999999999998312, -0.5150000000000000133 ) ) ;
#3132=ORIENTED_EDGE ( 'NONE', *, *, #5321, .T. ) ;
#3138=EDGE_CURVE ( 'NONE', #1403, #4174, #1674, .T. ) ;
#3142=ORIENTED_EDGE ( 'NONE', *, *, #1360, .T. ) ;
#3159=DIRECTION ( 'NONE',  ( 1.000000000000000000, 0.000000000000000000, 0.000000000000000000 ) ) ;
#3168=ORIENTED_EDGE ( 'NONE', *, *, #2864, .F. ) ;
#3175=LINE ( 'NONE', #1312, #3865 ) ;
#3179=CARTESIAN_POINT ( 'NONE',  ( 2.740000000000000213, 0.000000000000000000, 0.000000000000000000 ) ) ;
#3192=DIRECTION ( 'NONE',  ( 0.000000000000000000, -3.612465276695121047E-15, 1.000000000000000000 ) ) ;
#3202=LINE ( 'NONE', #4200, #704 ) ;
#3211=CIRCLE ( 'NONE', #2510, 7.983406227920510467 ) ;
#3213=AXIS2_PLACEMENT_3D ( 'NONE', #1599, #4891, #2539 ) ;
#3220=VERTEX_POINT ( 'NONE', #3742 ) ;
#3223=AXIS2_PLACEMENT_3D ( 'NONE', #2131, #3989, #5840 ) ;
#3233=DIRECTION ( 'NONE',  ( 0.4461977533474923430, -0.8949343913984144638, 0.000000000000000000 ) ) ;
#3236=ORIENTED_EDGE ( 'NONE', *, *, #1148, .T. ) ;
#3237=CARTESIAN_POINT ( 'NONE',  ( 0.3074992278157369086, -2.196686566159251619, -2.690165171976911629E-16 ) ) ;
#3238=DIRECTION ( 'NONE',  ( 0.8949343913984143528, 0.4461977533474922875, 0.000000000000000000 ) ) ;
#3242=CIRCLE ( 'NONE', #4992, 8.000000000000000000 ) ;
#3248=EDGE_CURVE ( 'NONE', #4039, #1741, #925, .T. ) ;
#3251=CARTESIAN_POINT ( 'NONE',  ( 2.740000000000000213, 0.000000000000000000, 0.000000000000000000 ) ) ;
#3253=FACE_OUTER_BOUND ( 'NONE', #3763, .T. ) ;
#3272=VERTEX_POINT ( 'NONE', #236 ) ;
#3287=EDGE_CURVE ( 'NONE', #2788, #4005, #3115, .T. ) ;
#3291=DIRECTION ( 'NONE',  ( 0.000000000000000000, 3.490239007934759657E-15, -1.000000000000000000 ) ) ;
#3301=CARTESIAN_POINT ( 'NONE',  ( 0.06760930072668812352, 0.5150000000000032330, -0.9010842325122888630 ) ) ;
#3302=AXIS2_PLACEMENT_3D ( 'NONE', #4331, #3507, #4909 ) ;
#3305=CIRCLE ( 'NONE', #2726, 4.556291390728477886 ) ;
#3312=ORIENTED_EDGE ( 'NONE', *, *, #1842, .T. ) ;
#3315=CIRCLE ( 'NONE', #2832, 0.4499999999999985678 ) ;
#3317=DIRECTION ( 'NONE',  ( 0.000000000000000000, 0.000000000000000000, 1.000000000000000000 ) ) ;
#3339=VECTOR ( 'NONE', #516, 1000.000000000000000 ) ;
#3351=EDGE_CURVE ( 'NONE', #3979, #553, #4073, .T. ) ;
#3354=CARTESIAN_POINT ( 'NONE',  ( 0.06760930072668812352, 0.5150000000000032330, -0.9010842325122888630 ) ) ;
#3358=DIRECTION ( 'NONE',  ( 0.4461977533474923430, -0.8949343913984144638, 0.000000000000000000 ) ) ;
#3365=CARTESIAN_POINT ( 'NONE',  ( 2.740000000000000213, -0.9838866223905674557, -0.5150000000000000133 ) ) ;
#3374=ORIENTED_EDGE ( 'NONE', *, *, #2160, .F. ) ;
#3376=CARTESIAN_POINT ( 'NONE',  ( 2.740000000000000213, 0.5150000000000035660, -0.9838866223905657904 ) ) ;
#3378=ORIENTED_EDGE ( 'NONE', *, *, #97, .F. ) ;
#3388=CARTESIAN_POINT ( 'NONE',  ( 8.000000000000000000, -4.837354856632045452E-15, -0.5150000000000000133 ) ) ;
#3391=DIRECTION ( 'NONE',  ( 0.000000000000000000, -1.224646799147353207E-16, 1.000000000000000000 ) ) ;
#3409=CARTESIAN_POINT ( 'NONE',  ( 2.740000000000000213, -0.5149999999999973488, -0.6774776749089248540 ) ) ;
#3418=EDGE_LOOP ( 'NONE', ( #2590, #219, #3864, #3475 ) ) ;
#3422=DIRECTION ( 'NONE',  ( 1.007709689656716815E-16, 1.153406566473941260E-16, -1.000000000000000000 ) ) ;
#3432=DIRECTION ( 'NONE',  ( 0.000000000000000000, 1.000000000000000000, 1.224646799147353207E-16 ) ) ;
#3447=DIRECTION ( 'NONE',  ( 0.8949343913984144638, 0.4461977533474923430, 0.000000000000000000 ) ) ;
#3450=DIRECTION ( 'NONE',  ( 0.4461977533473793778, 0.8949343913984707521, -1.884057886186824495E-16 ) ) ;
#3453=DIRECTION ( 'NONE',  ( 0.8949343913984143528, -1.557891129246500526E-15, 0.4461977533474922875 ) ) ;
#3469=ADVANCED_FACE ( 'NONE', ( #418 ), #2728, .F. ) ;
#3471=ORIENTED_EDGE ( 'NONE', *, *, #2316, .F. ) ;
#3475=ORIENTED_EDGE ( 'NONE', *, *, #4093, .T. ) ;
#3481=CARTESIAN_POINT ( 'NONE',  ( 2.740000000000000213, 0.9838866223910003317, 0.5149999999999999023 ) ) ;
#3483=ORIENTED_EDGE ( 'NONE', *, *, #1053, .F. ) ;
#3485=ORIENTED_EDGE ( 'NONE', *, *, #1688, .T. ) ;
#3489=CIRCLE ( 'NONE', #4654, 2.700000000000000178 ) ;
#3490=VECTOR ( 'NONE', #4457, 1000.000000000000000 ) ;
#3497=ORIENTED_EDGE ( 'NONE', *, *, #2460, .F. ) ;
#3507=DIRECTION ( 'NONE',  ( -1.000000000000000000, -0.000000000000000000, -0.000000000000000000 ) ) ;
#3510=ORIENTED_EDGE ( 'NONE', *, *, #2578, .F. ) ;
#3512=VECTOR ( 'NONE', #4221, 1000.000000000000000 ) ;
#3520=ADVANCED_FACE ( 'NONE', ( #5864 ), #3119, .F. ) ;
#3527=CARTESIAN_POINT ( 'NONE',  ( 0.000000000000000000, 0.000000000000000000, 0.000000000000000000 ) ) ;
#3530=ORIENTED_EDGE ( 'NONE', *, *, #320, .F. ) ;
#3538=EDGE_CURVE ( 'NONE', #3272, #2059, #4188, .T. ) ;
#3551=EDGE_CURVE ( 'NONE', #1830, #2555, #3079, .T. ) ;
#3552=ORIENTED_EDGE ( 'NONE', *, *, #907, .T. ) ;
#3554=DIRECTION ( 'NONE',  ( 0.000000000000000000, -1.000000000000000000, 0.000000000000000000 ) ) ;
#3555=CIRCLE ( 'NONE', #4813, 0.8509999999999999787 ) ;
#3569=CARTESIAN_POINT ( 'NONE',  ( 3.900000000000000799, 0.000000000000000000, 2.500000000000000000 ) ) ;
#3574=( NAMED_UNIT ( * ) SI_UNIT ( $, .STERADIAN. ) SOLID_ANGLE_UNIT ( ) );
#3584=AXIS2_PLACEMENT_3D ( 'NONE', #4792, #659, #2083 ) ;
#3585=VERTEX_POINT ( 'NONE', #3237 ) ;
#3587=EDGE_CURVE ( 'NONE', #2197, #3605, #4649, .T. ) ;
#3588=FACE_OUTER_BOUND ( 'NONE', #4795, .T. ) ;
#3594=EDGE_LOOP ( 'NONE', ( #1372, #2329 ) ) ;
#3601=FACE_OUTER_BOUND ( 'NONE', #32, .T. ) ;
#3605=VERTEX_POINT ( 'NONE', #2288 ) ;
#3606=AXIS2_PLACEMENT_3D ( 'NONE', #2781, #1892, #473 ) ;
#3607=PLANE ( 'NONE',  #1874 ) ;
#3619=CARTESIAN_POINT ( 'NONE',  ( -25.39999999999996305, 3.061616997868383141E-16, -2.500000000000000000 ) ) ;
#3621=EDGE_LOOP ( 'NONE', ( #4610, #744, #944, #2402 ) ) ;
#3628=EDGE_CURVE ( 'NONE', #2324, #3220, #5622, .T. ) ;
#3630=VERTEX_POINT ( 'NONE', #4889 ) ;
#3640=EDGE_LOOP ( 'NONE', ( #3853, #5019, #3103, #1801, #5789, #3014, #4719 ) ) ;
#3646=AXIS2_PLACEMENT_3D ( 'NONE', #1326, #4528, #3192 ) ;
#3649=ORIENTED_EDGE ( 'NONE', *, *, #2578, .T. ) ;
#3654=DIRECTION ( 'NONE',  ( 0.000000000000000000, 0.000000000000000000, 1.000000000000000000 ) ) ;
#3656=EDGE_LOOP ( 'NONE', ( #282, #2944 ) ) ;
#3658=ORIENTED_EDGE ( 'NONE', *, *, #5903, .F. ) ;
#3660=EDGE_CURVE ( 'NONE', #4439, #2598, #4400, .T. ) ;
#3661=DIRECTION ( 'NONE',  ( -0.000000000000000000, 0.000000000000000000, 1.000000000000000000 ) ) ;
#3667=CARTESIAN_POINT ( 'NONE',  ( 0.06760930072668894231, -0.9010842325122929708, -0.5150000000000000133 ) ) ;
#3669=CARTESIAN_POINT ( 'NONE',  ( 2.740000000000000213, 0.5150000000000024558, -0.6774776749089207462 ) ) ;
#3670=CARTESIAN_POINT ( 'NONE',  ( 3.900000000000000799, 0.000000000000000000, 0.000000000000000000 ) ) ;
#3674=PLANE ( 'NONE',  #517 ) ;
#3687=EDGE_CURVE ( 'NONE', #1480, #3012, #591, .T. ) ;
#3693=LINE ( 'NONE', #4271, #4863 ) ;
#3695=AXIS2_PLACEMENT_3D ( 'NONE', #3481, #2476, #182 ) ;
#3698=DIRECTION ( 'NONE',  ( 0.000000000000000000, 0.000000000000000000, 1.000000000000000000 ) ) ;
#3701=AXIS2_PLACEMENT_3D ( 'NONE', #5532, #1376, #4205 ) ;
#3704=DIRECTION ( 'NONE',  ( 0.8949343913984707521, 0.000000000000000000, -0.4461977533473793223 ) ) ;
#3735=PLANE ( 'NONE',  #3910 ) ;
#3742=CARTESIAN_POINT ( 'NONE',  ( 0.3226060873438244547, -2.189154565102686245, -0.5150000000000000133 ) ) ;
#3757=DIRECTION ( 'NONE',  ( -1.000000000000000000, -0.000000000000000000, -0.000000000000000000 ) ) ;
#3759=VECTOR ( 'NONE', #2615, 1000.000000000000000 ) ;
#3763=EDGE_LOOP ( 'NONE', ( #3483, #4871, #5166, #3940, #2074, #752, #5198, #3378, #773, #409, #3824, #5635, #5065 ) ) ;
#3772=EDGE_LOOP ( 'NONE', ( #4998, #44, #5535, #4796 ) ) ;
#3783=CARTESIAN_POINT ( 'NONE',  ( 3.900000000000000799, 0.000000000000000000, 0.000000000000000000 ) ) ;
#3786=AXIS2_PLACEMENT_3D ( 'NONE', #5281, #2475, #181 ) ;
#3790=CARTESIAN_POINT ( 'NONE',  ( 2.740000000000000213, 0.000000000000000000, 0.000000000000000000 ) ) ;
#3792=AXIS2_PLACEMENT_3D ( 'NONE', #1080, #249, #2017 ) ;
#3798=EDGE_LOOP ( 'NONE', ( #1928, #3909, #5892, #679 ) ) ;
#3800=DIRECTION ( 'NONE',  ( 0.000000000000000000, -3.491481338843133355E-15, 1.000000000000000000 ) ) ;
#3802=DIRECTION ( 'NONE',  ( 0.4461977533473793778, 0.8949343913984707521, -1.884057886186824495E-16 ) ) ;
#3822=CARTESIAN_POINT ( 'NONE',  ( 2.740000000000000213, 0.9838866223910001096, -0.5150000000000001243 ) ) ;
#3823=DIRECTION ( 'NONE',  ( 0.000000000000000000, 0.000000000000000000, 1.000000000000000000 ) ) ;
#3824=ORIENTED_EDGE ( 'NONE', *, *, #405, .F. ) ;
#3828=CARTESIAN_POINT ( 'NONE',  ( 0.000000000000000000, -2.349999999999997424, 0.5149999999999992362 ) ) ;
#3833=CIRCLE ( 'NONE', #3646, 7.983406227920510467 ) ;
#3845=DIRECTION ( 'NONE',  ( 1.000000000000000000, 0.000000000000000000, 0.000000000000000000 ) ) ;
#3853=ORIENTED_EDGE ( 'NONE', *, *, #5321, .F. ) ;
#3856=DIRECTION ( 'NONE',  ( 1.007709689656716815E-16, 1.153406566473941260E-16, -1.000000000000000000 ) ) ;
#3863=DIRECTION ( 'NONE',  ( 0.8949343913984144638, 0.4461977533474923430, 0.000000000000000000 ) ) ;
#3864=ORIENTED_EDGE ( 'NONE', *, *, #3628, .T. ) ;
#3865=VECTOR ( 'NONE', #5028, 1000.000000000000114 ) ;
#3866=ADVANCED_FACE ( 'NONE', ( #1499 ), #27, .T. ) ;
#3891=EDGE_LOOP ( 'NONE', ( #192, #5076, #2087, #664, #1313 ) ) ;
#3896=CARTESIAN_POINT ( 'NONE',  ( 19.70000000000000284, 0.000000000000000000, 0.000000000000000000 ) ) ;
#3898=DIRECTION ( 'NONE',  ( 0.000000000000000000, 1.000000000000000000, 1.086455722314322026E-16 ) ) ;
#3901=CARTESIAN_POINT ( 'NONE',  ( 2.740000000000000213, 0.6774776749089228556, 0.5149999999999997913 ) ) ;
#3903=CARTESIAN_POINT ( 'NONE',  ( 0.06760930072668799862, 0.5149999999999969047, 0.9010842325122926377 ) ) ;
#3909=ORIENTED_EDGE ( 'NONE', *, *, #1419, .F. ) ;
#3910=AXIS2_PLACEMENT_3D ( 'NONE', #5057, #5583, #4071 ) ;
#3932=DIRECTION ( 'NONE',  ( 0.000000000000000000, 0.000000000000000000, 1.000000000000000000 ) ) ;
#3933=CARTESIAN_POINT ( 'NONE',  ( 0.000000000000000000, -2.349999999999999201, 0.5149999999999992362 ) ) ;
#3936=ORIENTED_EDGE ( 'NONE', *, *, #3687, .T. ) ;
#3940=ORIENTED_EDGE ( 'NONE', *, *, #280, .T. ) ;
#3944=CARTESIAN_POINT ( 'NONE',  ( 1.794155980045909482, 0.000000000000000000, 4.300000000000001599 ) ) ;
#3949=PLANE ( 'NONE',  #3009 ) ;
#3961=DIRECTION ( 'NONE',  ( -1.000000000000000000, 0.000000000000000000, -0.000000000000000000 ) ) ;
#3975=EDGE_CURVE ( 'NONE', #5342, #171, #4970, .T. ) ;
#3979=VERTEX_POINT ( 'NONE', #770 ) ;
#3987=VECTOR ( 'NONE', #174, 1000.000000000000114 ) ;
#3988=AXIS2_PLACEMENT_3D ( 'NONE', #5929, #3111, #4937 ) ;
#3989=DIRECTION ( 'NONE',  ( -1.000000000000000000, -0.000000000000000000, -0.000000000000000000 ) ) ;
#3991=ORIENTED_EDGE ( 'NONE', *, *, #198, .T. ) ;
#4005=VERTEX_POINT ( 'NONE', #5005 ) ;
#4007=ORIENTED_EDGE ( 'NONE', *, *, #3351, .T. ) ;
#4017=EDGE_LOOP ( 'NONE', ( #420, #1634, #193, #4480 ) ) ;
#4020=VERTEX_POINT ( 'NONE', #5328 ) ;
#4032=DIRECTION ( 'NONE',  ( -1.000000000000000000, -0.000000000000000000, -0.000000000000000000 ) ) ;
#4039=VERTEX_POINT ( 'NONE', #5506 ) ;
#4040=CARTESIAN_POINT ( 'NONE',  ( 2.740000000000000213, 0.9838866223910003317, 0.5149999999999999023 ) ) ;
#4045=DIRECTION ( 'NONE',  ( 0.000000000000000000, 1.000000000000000000, 1.086455722314322026E-16 ) ) ;
#4052=DIRECTION ( 'NONE',  ( 0.000000000000000000, 0.000000000000000000, 1.000000000000000000 ) ) ;
#4056=( NAMED_UNIT ( * ) SI_UNIT ( $, .STERADIAN. ) SOLID_ANGLE_UNIT ( ) );
#4058=ADVANCED_BREP_SHAPE_REPRESENTATION ( '', ( #189, #5080 ), #5845 ) ;
#4071=DIRECTION ( 'NONE',  ( -0.000000000000000000, 0.000000000000000000, 1.000000000000000000 ) ) ;
#4073=CIRCLE ( 'NONE', #2427, 2.500000000000000000 ) ;
#4079=ORIENTED_EDGE ( 'NONE', *, *, #1449, .F. ) ;
#4086=DIRECTION ( 'NONE',  ( 1.000000000000000000, 0.000000000000000000, 0.000000000000000000 ) ) ;
#4093=EDGE_CURVE ( 'NONE', #3220, #4439, #4570, .T. ) ;
#4094=DIRECTION ( 'NONE',  ( 0.000000000000000000, 0.000000000000000000, 1.000000000000000000 ) ) ;
#4109=DIRECTION ( 'NONE',  ( 1.000000000000000000, 0.000000000000000000, 0.000000000000000000 ) ) ;
#4112=DIRECTION ( 'NONE',  ( -1.000000000000000000, -0.000000000000000000, -0.000000000000000000 ) ) ;
#4114=FACE_OUTER_BOUND ( 'NONE', #5790, .T. ) ;
#4123=CARTESIAN_POINT ( 'NONE',  ( 0.3074992278157512304, 2.196686566159293807, -2.407412430484044816E-32 ) ) ;
#4125=CARTESIAN_POINT ( 'NONE',  ( 0.000000000000000000, 2.349999999999998312, -0.5150000000000000133 ) ) ;
#4138=EDGE_CURVE ( 'NONE', #2197, #4461, #4381, .T. ) ;
#4143=DIRECTION ( 'NONE',  ( 0.8949343913984706411, -0.4461977533473793223, 7.082407382381129037E-17 ) ) ;
#4155=DIRECTION ( 'NONE',  ( 1.000000000000000000, 0.000000000000000000, 0.000000000000000000 ) ) ;
#4161=ORIENTED_EDGE ( 'NONE', *, *, #537, .F. ) ;
#4166=ADVANCED_FACE ( 'NONE', ( #4114 ), #4577, .T. ) ;
#4170=LINE ( 'NONE', #443, #98 ) ;
#4174=VERTEX_POINT ( 'NONE', #1315 ) ;
#4175=EDGE_LOOP ( 'NONE', ( #3530, #3132, #5427, #78, #2909, #1636, #2275 ) ) ;
#4184=ORIENTED_EDGE ( 'NONE', *, *, #1053, .T. ) ;
#4185=EDGE_CURVE ( 'NONE', #171, #2598, #5253, .T. ) ;
#4188=CIRCLE ( 'NONE', #3223, 4.750000000000000000 ) ;
#4193=ORIENTED_EDGE ( 'NONE', *, *, #3138, .F. ) ;
#4194=TOROIDAL_SURFACE ( 'NONE', #4977, 2.700000000000000178, 0.2000000000000000111 ) ;
#4195=FACE_OUTER_BOUND ( 'NONE', #3640, .T. ) ;
#4198=ORIENTED_EDGE ( 'NONE', *, *, #1714, .T. ) ;
#4200=CARTESIAN_POINT ( 'NONE',  ( 3.016506661494197328, 0.000000000000000000, 7.007546303702493782E-17 ) ) ;
#4204=ORIENTED_EDGE ( 'NONE', *, *, #5738, .T. ) ;
#4205=DIRECTION ( 'NONE',  ( 0.000000000000000000, 0.000000000000000000, 1.000000000000000000 ) ) ;
#4221=DIRECTION ( 'NONE',  ( 0.000000000000000000, 1.000000000000000000, 0.000000000000000000 ) ) ;
#4230=CONICAL_SURFACE ( 'NONE', #837, 0.8509999999999999787, 0.06981317007976602096 ) ;
#4234=AXIS2_PLACEMENT_3D ( 'NONE', #3084, #1229, #2174 ) ;
#4238=DIRECTION ( 'NONE',  ( 0.000000000000000000, -1.000000000000000000, -3.702006032529638986E-15 ) ) ;
#4266=DIRECTION ( 'NONE',  ( 0.4461977533473793778, -2.936240938438015166E-15, 0.8949343913984707521 ) ) ;
#4268=CARTESIAN_POINT ( 'NONE',  ( 2.740000000000000213, -0.6774776749089230776, 0.5149999999999995692 ) ) ;
#4271=CARTESIAN_POINT ( 'NONE',  ( 2.740000000000000213, -0.9838866223905674557, -0.5150000000000000133 ) ) ;
#4278=VERTEX_POINT ( 'NONE', #3669 ) ;
#4301=FACE_OUTER_BOUND ( 'NONE', #4625, .T. ) ;
#4310=DIRECTION ( 'NONE',  ( 0.000000000000000000, -1.000000000000000000, -1.652937667529658626E-16 ) ) ;
#4318=DIRECTION ( 'NONE',  ( -1.000000000000000000, -0.000000000000000000, -0.000000000000000000 ) ) ;
#4319=ADVANCED_FACE ( 'NONE', ( #1759 ), #5020, .T. ) ;
#4322=AXIS2_PLACEMENT_3D ( 'NONE', #1391, #5424, #5079 ) ;
#4331=CARTESIAN_POINT ( 'NONE',  ( 1.424271237134740131, 0.000000000000000000, 0.000000000000000000 ) ) ;
#4334=ORIENTED_EDGE ( 'NONE', *, *, #938, .F. ) ;
#4343=ORIENTED_EDGE ( 'NONE', *, *, #3628, .F. ) ;
#4345=CARTESIAN_POINT ( 'NONE',  ( 0.06760930072668806801, -4.837354856632045452E-15, 0.000000000000000000 ) ) ;
#4347=ORIENTED_EDGE ( 'NONE', *, *, #3287, .F. ) ;
#4350=DIRECTION ( 'NONE',  ( 0.000000000000000000, -1.000000000000000000, -3.491481338843133355E-15 ) ) ;
#4358=DIRECTION ( 'NONE',  ( -1.000000000000000000, -0.000000000000000000, -0.000000000000000000 ) ) ;
#4360=CARTESIAN_POINT ( 'NONE',  ( 8.000000000000000000, -4.896755294805453861E-15, 0.5150000000000000133 ) ) ;
#4368=DIRECTION ( 'NONE',  ( 0.8949343913984143528, -1.557891129246500526E-15, 0.4461977533474922875 ) ) ;
#4370=EDGE_CURVE ( 'NONE', #1472, #4005, #3315, .T. ) ;
#4381=CIRCLE ( 'NONE', #2733, 1.037871761867652065 ) ;
#4383=CONICAL_SURFACE ( 'NONE', #4677, 0.8509999999999999787, 0.06981317007976602096 ) ;
#4399=EDGE_CURVE ( 'NONE', #2059, #3630, #4531, .T. ) ;
#4400=LINE ( 'NONE', #5239, #2431 ) ;
#4403=CARTESIAN_POINT ( 'NONE',  ( 2.740000000000000213, 0.000000000000000000, 0.000000000000000000 ) ) ;
#4415=LINE ( 'NONE', #3619, #777 ) ;
#4418=CIRCLE ( 'NONE', #4322, 4.556291390728477886 ) ;
#4419=CARTESIAN_POINT ( 'NONE',  ( 3.699999999999998401, 0.000000000000000000, 4.750000000000000000 ) ) ;
#4428=FACE_OUTER_BOUND ( 'NONE', #4448, .T. ) ;
#4431=FACE_OUTER_BOUND ( 'NONE', #433, .T. ) ;
#4439=VERTEX_POINT ( 'NONE', #8 ) ;
#4448=EDGE_LOOP ( 'NONE', ( #2130, #1831, #999, #1124 ) ) ;
#4453=ORIENTED_EDGE ( 'NONE', *, *, #938, .T. ) ;
#4457=DIRECTION ( 'NONE',  ( 0.000000000000000000, 3.656775105596099119E-15, -1.000000000000000000 ) ) ;
#4458=CYLINDRICAL_SURFACE ( 'NONE', #2046, 4.749999999999999112 ) ;
#4460=AXIS2_PLACEMENT_3D ( 'NONE', #110, #3802, #5654 ) ;
#4461=VERTEX_POINT ( 'NONE', #2417 ) ;
#4462=( NAMED_UNIT ( * ) PLANE_ANGLE_UNIT ( ) SI_UNIT ( $, .RADIAN. ) );
#4474=ORIENTED_EDGE ( 'NONE', *, *, #1615, .F. ) ;
#4480=ORIENTED_EDGE ( 'NONE', *, *, #1842, .F. ) ;
#4481=CIRCLE ( 'NONE', #4964, 7.864440107515430434 ) ;
#4484=DIRECTION ( 'NONE',  ( 0.000000000000000000, 0.000000000000000000, 1.000000000000000000 ) ) ;
#4486=DIRECTION ( 'NONE',  ( -0.3090169943749412895, 1.164708318489094811E-16, -0.9510565162951555296 ) ) ;
#4494=UNCERTAINTY_MEASURE_WITH_UNIT (LENGTH_MEASURE( 1.000000000000000082E-05 ), #4587, 'distance_accuracy_value', 'NONE');
#4500=ORIENTED_EDGE ( 'NONE', *, *, #2160, .T. ) ;
#4501=CARTESIAN_POINT ( 'NONE',  ( 1.794155980045909482, 5.265981236333621429E-16, -4.300000000000001599 ) ) ;
#4505=LINE ( 'NONE', #1184, #875 ) ;
#4506=ORIENTED_EDGE ( 'NONE', *, *, #3248, .T. ) ;
#4514=EDGE_CURVE ( 'NONE', #1071, #635, #1508, .T. ) ;
#4521=CARTESIAN_POINT ( 'NONE',  ( 3.699999999999998401, 0.000000000000000000, 0.000000000000000000 ) ) ;
#4523=PLANE ( 'NONE',  #308 ) ;
#4524=CONICAL_SURFACE ( 'NONE', #65, 0.8509999999999999787, 0.06981317007976602096 ) ;
#4528=DIRECTION ( 'NONE',  ( 1.007709689656716938E-16, 1.000000000000000000, 3.606821995490528048E-15 ) ) ;
#4531=LINE ( 'NONE', #2152, #5355 ) ;
#4533=CARTESIAN_POINT ( 'NONE',  ( 0.9586399445693778443, 0.8293189044373067143, -0.5150000000000000133 ) ) ;
#4535=ORIENTED_EDGE ( 'NONE', *, *, #1242, .T. ) ;
#4542=ORIENTED_EDGE ( 'NONE', *, *, #198, .F. ) ;
#4546=ADVANCED_FACE ( 'NONE', ( #3253 ), #38, .T. ) ;
#4548=CARTESIAN_POINT ( 'NONE',  ( 0.3226060873438262311, 0.5150000000000077849, -2.189154565102684025 ) ) ;
#4550=CARTESIAN_POINT ( 'NONE',  ( 3.900000000000000799, 0.000000000000000000, 2.700000000000000178 ) ) ;
#4553=DIRECTION ( 'NONE',  ( -1.000000000000000000, -0.000000000000000000, -0.000000000000000000 ) ) ;
#4560=AXIS2_PLACEMENT_3D ( 'NONE', #3822, #5196, #4833 ) ;
#4561=CARTESIAN_POINT ( 'NONE',  ( 0.06760930072668842883, -0.5149999999999961275, -0.9010842325122929708 ) ) ;
#4566=CARTESIAN_POINT ( 'NONE',  ( 8.000000000000000000, -4.837354856632045452E-15, 0.000000000000000000 ) ) ;
#4569=DIRECTION ( 'NONE',  ( -1.000000000000000000, -0.000000000000000000, -0.000000000000000000 ) ) ;
#4570=LINE ( 'NONE', #4658, #5627 ) ;
#4577=TOROIDAL_SURFACE ( 'NONE', #3701, 4.300000000000001599, 0.4499999999999985678 ) ;
#4578=PLANE ( 'NONE',  #5802 ) ;
#4584=CONICAL_SURFACE ( 'NONE', #3025, 0.8509999999999999787, 0.06981317007976602096 ) ;
#4587=( LENGTH_UNIT ( ) NAMED_UNIT ( * ) SI_UNIT ( .MILLI., .METRE. ) );
#4589=CARTESIAN_POINT ( 'NONE',  ( 0.9586399445693646326, 0.8293189044373081575, 0.5149999999999996803 ) ) ;
#4590=AXIS2_PLACEMENT_3D ( 'NONE', #4566, #1821, #4109 ) ;
#4592=ORIENTED_EDGE ( 'NONE', *, *, #4370, .T. ) ;
#4601=ORIENTED_EDGE ( 'NONE', *, *, #3660, .F. ) ;
#4610=ORIENTED_EDGE ( 'NONE', *, *, #3013, .T. ) ;
#4619=ADVANCED_FACE ( 'NONE', ( #4431 ), #2571, .F. ) ;
#4623=FACE_OUTER_BOUND ( 'NONE', #3621, .T. ) ;
#4625=EDGE_LOOP ( 'NONE', ( #1090, #5116 ) ) ;
#4630=EDGE_CURVE ( 'NONE', #2264, #1983, #2112, .T. ) ;
#4633=EDGE_LOOP ( 'NONE', ( #2113, #4535, #4184, #4695, #4343, #167, #321, #3485, #4161, #206, #1884, #5715, #1952 ) ) ;
#4649=B_SPLINE_CURVE_WITH_KNOTS ( 'NONE', 3,
 ( #3903, #5755, #2051, #1533 ),
 .UNSPECIFIED., .F., .F.,
 ( 4, 4 ),
 ( 0.001586480563516616538, 0.004268227385920363680 ),
 .UNSPECIFIED. ) ;
#4654=AXIS2_PLACEMENT_3D ( 'NONE', #1431, #423, #1379 ) ;
#4655=AXIS2_PLACEMENT_3D ( 'NONE', #213, #3422, #269 ) ;
#4658=CARTESIAN_POINT ( 'NONE',  ( 0.000000000000000000, -2.349999999999999201, -0.5150000000000000133 ) ) ;
#4661=EDGE_LOOP ( 'NONE', ( #2572, #990, #1171, #3168 ) ) ;
#4665=LINE ( 'NONE', #2863, #5896 ) ;
#4677=AXIS2_PLACEMENT_3D ( 'NONE', #4403, #4759, #3932 ) ;
#4683=AXIS2_PLACEMENT_3D ( 'NONE', #2184, #5428, #5403 ) ;
#4689=CARTESIAN_POINT ( 'NONE',  ( 0.3226060873438244547, -2.189154565102685801, 0.5149999999999992362 ) ) ;
#4691=ADVANCED_FACE ( 'NONE', ( #1170 ), #4794, .T. ) ;
#4695=ORIENTED_EDGE ( 'NONE', *, *, #5133, .T. ) ;
#4704=CARTESIAN_POINT ( 'NONE',  ( 0.06760930072668894231, -0.9010842325122859764, 0.5149999999999992362 ) ) ;
#4712=APPLICATION_CONTEXT ( 'automotive_design' ) ;
#4713=ORIENTED_EDGE ( 'NONE', *, *, #907, .F. ) ;
#4716=AXIS2_PLACEMENT_3D ( 'NONE', #1030, #521, #2369 ) ;
#4719=ORIENTED_EDGE ( 'NONE', *, *, #1615, .T. ) ;
#4723=FACE_OUTER_BOUND ( 'NONE', #2576, .T. ) ;
#4724=EDGE_CURVE ( 'NONE', #3012, #199, #2252, .T. ) ;
#4725=DIRECTION ( 'NONE',  ( 1.000000000000000000, 0.000000000000000000, 0.000000000000000000 ) ) ;
#4728=ORIENTED_EDGE ( 'NONE', *, *, #1242, .F. ) ;
#4729=ADVANCED_FACE ( 'NONE', ( #843 ), #4523, .T. ) ;
#4732=CARTESIAN_POINT ( 'NONE',  ( 1.424271237134740131, 4.556291390728479662, 0.000000000000000000 ) ) ;
#4737=EDGE_CURVE ( 'NONE', #140, #2788, #3305, .T. ) ;
#4740=CARTESIAN_POINT ( 'NONE',  ( 8.000000000000000000, 0.5150000000000000133, 1.798112889504231112E-15 ) ) ;
#4743=DIRECTION ( 'NONE',  ( -1.000000000000000000, -0.000000000000000000, -0.000000000000000000 ) ) ;
#4746=CARTESIAN_POINT ( 'NONE',  ( 1.424271237134740131, 0.000000000000000000, 4.556291390728477886 ) ) ;
#4747=AXIS2_PLACEMENT_3D ( 'NONE', #103, #1939, #1587 ) ;
#4759=DIRECTION ( 'NONE',  ( -1.000000000000000000, -0.000000000000000000, -0.000000000000000000 ) ) ;
#4778=ORIENTED_EDGE ( 'NONE', *, *, #4923, .T. ) ;
#4792=CARTESIAN_POINT ( 'NONE',  ( 1.794155980045911036, 0.000000000000000000, 0.000000000000000000 ) ) ;
#4794=PLANE ( 'NONE',  #2918 ) ;
#4795=EDGE_LOOP ( 'NONE', ( #3991, #1060, #2889, #2190 ) ) ;
#4796=ORIENTED_EDGE ( 'NONE', *, *, #5072, .T. ) ;
#4798=PRODUCT ( 'pan head cross recess screw_iso_ISO 7045 - M5 x 16 - Z - 16N', 'pan head cross recess screw_iso_ISO 7045 - M5 x 16 - Z - 16N', '', ( #1106 ) ) ;
#4810=EDGE_CURVE ( 'NONE', #5067, #1750, #5152, .T. ) ;
#4813=AXIS2_PLACEMENT_3D ( 'NONE', #1456, #1005, #5737 ) ;
#4826=EDGE_LOOP ( 'NONE', ( #2093, #4007, #3312, #3552 ) ) ;
#4831=DIRECTION ( 'NONE',  ( 0.000000000000000000, 0.000000000000000000, 1.000000000000000000 ) ) ;
#4833=DIRECTION ( 'NONE',  ( -0.000000000000000000, 0.000000000000000000, 1.000000000000000000 ) ) ;
#4843=CARTESIAN_POINT ( 'NONE',  ( 2.740000000000000213, 0.000000000000000000, 0.000000000000000000 ) ) ;
#4849=CARTESIAN_POINT ( 'NONE',  ( 2.740000000000000213, -0.5149999999999973488, -0.6774776749089248540 ) ) ;
#4863=VECTOR ( 'NONE', #954, 1000.000000000000000 ) ;
#4868=PLANE ( 'NONE',  #4560 ) ;
#4871=ORIENTED_EDGE ( 'NONE', *, *, #2460, .T. ) ;
#4872=DIRECTION ( 'NONE',  ( 1.000000000000000000, 0.000000000000000000, 0.000000000000000000 ) ) ;
#4876=CARTESIAN_POINT ( 'NONE',  ( 3.700000000000000178, 3.306546357697853733E-16, -2.700000000000000178 ) ) ;
#4889=CARTESIAN_POINT ( 'NONE',  ( 1.794155980045911036, 0.000000000000000000, 4.749999999999999112 ) ) ;
#4891=DIRECTION ( 'NONE',  ( -1.000000000000000000, -0.000000000000000000, -0.000000000000000000 ) ) ;
#4909=DIRECTION ( 'NONE',  ( 0.000000000000000000, 0.000000000000000000, 1.000000000000000000 ) ) ;
#4916=CARTESIAN_POINT ( 'NONE',  ( 0.06760930072668842883, -0.5149999999999961275, -0.9010842325122929708 ) ) ;
#4919=PRODUCT_DEFINITION_CONTEXT ( 'detailed design', #4712, 'design' ) ;
#4923=EDGE_CURVE ( 'NONE', #4439, #1983, #3693, .T. ) ;
#4926=AXIS2_PLACEMENT_3D ( 'NONE', #1806, #4086, #2663 ) ;
#4934=CARTESIAN_POINT ( 'NONE',  ( 2.740000000000000213, 0.000000000000000000, 0.000000000000000000 ) ) ;
#4937=DIRECTION ( 'NONE',  ( 0.000000000000000000, 0.000000000000000000, 1.000000000000000000 ) ) ;
#4938=ORIENTED_EDGE ( 'NONE', *, *, #4630, .F. ) ;
#4939=LINE ( 'NONE', #3114, #2524 ) ;
#4964=AXIS2_PLACEMENT_3D ( 'NONE', #1595, #5657, #3447 ) ;
#4970=CIRCLE ( 'NONE', #3988, 0.8509999999999999787 ) ;
#4973=DIRECTION ( 'NONE',  ( -1.000000000000000000, -0.000000000000000000, -0.000000000000000000 ) ) ;
#4975=CARTESIAN_POINT ( 'NONE',  ( 2.740000000000000213, 1.042174426074397490E-16, -0.8509999999999999787 ) ) ;
#4977=AXIS2_PLACEMENT_3D ( 'NONE', #3670, #5523, #2424 ) ;
#4981=AXIS2_PLACEMENT_3D ( 'NONE', #1716, #2593, #362 ) ;
#4984=DIRECTION ( 'NONE',  ( -0.000000000000000000, 0.000000000000000000, 1.000000000000000000 ) ) ;
#4988=EDGE_LOOP ( 'NONE', ( #2760, #2754, #5889, #3497, #4728 ) ) ;
#4990=CIRCLE ( 'NONE', #2359, 2.500000000000000000 ) ;
#4992=AXIS2_PLACEMENT_3D ( 'NONE', #2507, #1698, #3432 ) ;
#4998=ORIENTED_EDGE ( 'NONE', *, *, #2316, .T. ) ;
#5005=CARTESIAN_POINT ( 'NONE',  ( 1.424271237134740131, 5.698459981794101142E-16, -4.556291390728477886 ) ) ;
#5006=ORIENTED_EDGE ( 'NONE', *, *, #1617, .T. ) ;
#5019=ORIENTED_EDGE ( 'NONE', *, *, #320, .T. ) ;
#5020=PLANE ( 'NONE',  #4683 ) ;
#5026=DIRECTION ( 'NONE',  ( 0.8949343913984143528, 0.4461977533474922875, 0.000000000000000000 ) ) ;
#5028=DIRECTION ( 'NONE',  ( 0.8949343913984143528, -1.699539276894113739E-15, 0.4461977533474921764 ) ) ;
#5033=ORIENTED_EDGE ( 'NONE', *, *, #2195, .T. ) ;
#5047=CIRCLE ( 'NONE', #4460, 7.864440107515625833 ) ;
#5048=ORIENTED_EDGE ( 'NONE', *, *, #1308, .T. ) ;
#5050=EDGE_CURVE ( 'NONE', #3605, #1563, #3112, .T. ) ;
#5054=CIRCLE ( 'NONE', #3213, 2.700000000000000178 ) ;
#5057=CARTESIAN_POINT ( 'NONE',  ( 2.740000000000000213, 0.9838866223910001096, -0.5150000000000001243 ) ) ;
#5065=ORIENTED_EDGE ( 'NONE', *, *, #5182, .T. ) ;
#5067=VERTEX_POINT ( 'NONE', #2933 ) ;
#5069=AXIS2_PLACEMENT_3D ( 'NONE', #5757, #2997, #3453 ) ;
#5072=EDGE_CURVE ( 'NONE', #342, #1588, #1131, .T. ) ;
#5076=ORIENTED_EDGE ( 'NONE', *, *, #4923, .F. ) ;
#5079=DIRECTION ( 'NONE',  ( 0.000000000000000000, 0.000000000000000000, 1.000000000000000000 ) ) ;
#5080=AXIS2_PLACEMENT_3D ( 'NONE', #3527, #4831, #667 ) ;
#5083=CARTESIAN_POINT ( 'NONE',  ( 1.849560077140141257, 0.7556913915602415655, -0.5150000000000000133 ) ) ;
#5095=ORIENTED_EDGE ( 'NONE', *, *, #1465, .F. ) ;
#5099=CARTESIAN_POINT ( 'NONE',  ( 0.000000000000000000, 0.5149999999999917977, 2.350000000000001865 ) ) ;
#5107=CARTESIAN_POINT ( 'NONE',  ( 7.345657149124969365, -5.313980200056029618E-16, -1.312408941149200148 ) ) ;
#5112=AXIS2_PLACEMENT_3D ( 'NONE', #136, #4318, #3317 ) ;
#5114=CIRCLE ( 'NONE', #1513, 7.864440107515625833 ) ;
#5116=ORIENTED_EDGE ( 'NONE', *, *, #3351, .F. ) ;
#5120=CARTESIAN_POINT ( 'NONE',  ( 8.000000000000000000, 0.5150000000000000133, 1.798112889504231112E-15 ) ) ;
#5130=DIRECTION ( 'NONE',  ( 0.000000000000000000, 0.000000000000000000, 1.000000000000000000 ) ) ;
#5132=EDGE_CURVE ( 'NONE', #2264, #1403, #5252, .T. ) ;
#5133=EDGE_CURVE ( 'NONE', #3585, #3220, #5726, .T. ) ;
#5147=ORIENTED_EDGE ( 'NONE', *, *, #5405, .F. ) ;
#5152=CIRCLE ( 'NONE', #2035, 0.2000000000000000944 ) ;
#5158=AXIS2_PLACEMENT_3D ( 'NONE', #3179, #4743, #3823 ) ;
#5159=LINE ( 'NONE', #598, #2776 ) ;
#5166=ORIENTED_EDGE ( 'NONE', *, *, #4737, .T. ) ;
#5170=ORIENTED_EDGE ( 'NONE', *, *, #5405, .T. ) ;
#5176=( NAMED_UNIT ( * ) PLANE_ANGLE_UNIT ( ) SI_UNIT ( $, .RADIAN. ) );
#5178=CARTESIAN_POINT ( 'NONE',  ( 0.9586399445693637444, -0.8293189044373081575, 0.5149999999999994582 ) ) ;
#5182=EDGE_CURVE ( 'NONE', #2264, #3585, #4481, .T. ) ;
#5196=DIRECTION ( 'NONE',  ( -1.000000000000000000, 0.000000000000000000, -0.000000000000000000 ) ) ;
#5198=ORIENTED_EDGE ( 'NONE', *, *, #4138, .F. ) ;
#5206=DIRECTION ( 'NONE',  ( -1.000000000000000000, -0.000000000000000000, -0.000000000000000000 ) ) ;
#5216=EDGE_CURVE ( 'NONE', #4461, #1830, #313, .T. ) ;
#5239=CARTESIAN_POINT ( 'NONE',  ( 2.740000000000000213, -0.9838866223905674557, -0.5150000000000000133 ) ) ;
#5252=CIRCLE ( 'NONE', #975, 7.983406227920510467 ) ;
#5253=CIRCLE ( 'NONE', #5158, 0.8509999999999999787 ) ;
#5260=PLANE ( 'NONE',  #5810 ) ;
#5278=CARTESIAN_POINT ( 'NONE',  ( 1.794155980045911036, 5.817072295949926440E-16, -4.749999999999999112 ) ) ;
#5281=CARTESIAN_POINT ( 'NONE',  ( -25.39999999999996305, 0.000000000000000000, 0.000000000000000000 ) ) ;
#5283=VERTEX_POINT ( 'NONE', #1656 ) ;
#5284=AXIS2_PLACEMENT_3D ( 'NONE', #2946, #42, #2393 ) ;
#5296=CIRCLE ( 'NONE', #1405, 1.037871761867652065 ) ;
#5298=ORIENTED_EDGE ( 'NONE', *, *, #4185, .F. ) ;
#5299=CIRCLE ( 'NONE', #5112, 0.8509999999999999787 ) ;
#5321=EDGE_CURVE ( 'NONE', #2852, #5342, #4939, .T. ) ;
#5324=AXIS2_PLACEMENT_3D ( 'NONE', #2439, #3019, #1651 ) ;
#5328=CARTESIAN_POINT ( 'NONE',  ( 0.3226060873438383325, 0.5149999999999923528, 2.189154565102733319 ) ) ;
#5331=ORIENTED_EDGE ( 'NONE', *, *, #405, .T. ) ;
#5342=VERTEX_POINT ( 'NONE', #4975 ) ;
#5355=VECTOR ( 'NONE', #371, 1000.000000000000000 ) ;
#5375=CYLINDRICAL_SURFACE ( 'NONE', #1485, 2.500000000000000000 ) ;
#5376=EDGE_LOOP ( 'NONE', ( #4334, #3658, #4079, #3471, #3142 ) ) ;
#5399=B_SPLINE_CURVE_WITH_KNOTS ( 'NONE', 3,
 ( #785, #431, #4589, #2729 ),
 .UNSPECIFIED., .F., .F.,
 ( 4, 4 ),
 ( 0.004656695506220394354, 0.007337072593346776264 ),
 .UNSPECIFIED. ) ;
#5403=DIRECTION ( 'NONE',  ( -0.000000000000000000, 0.000000000000000000, 1.000000000000000000 ) ) ;
#5404=DIRECTION ( 'NONE',  ( 0.000000000000000000, 0.000000000000000000, -1.000000000000000000 ) ) ;
#5405=EDGE_CURVE ( 'NONE', #2028, #1825, #787, .T. ) ;
#5423=( NAMED_UNIT ( * ) PLANE_ANGLE_UNIT ( ) SI_UNIT ( $, .RADIAN. ) );
#5424=DIRECTION ( 'NONE',  ( -1.000000000000000000, -0.000000000000000000, -0.000000000000000000 ) ) ;
#5427=ORIENTED_EDGE ( 'NONE', *, *, #3975, .T. ) ;
#5428=DIRECTION ( 'NONE',  ( -1.000000000000000000, 0.000000000000000000, -0.000000000000000000 ) ) ;
#5438=EDGE_CURVE ( 'NONE', #4174, #1983, #1572, .T. ) ;
#5440=VECTOR ( 'NONE', #4310, 1000.000000000000000 ) ;
#5442=CARTESIAN_POINT ( 'NONE',  ( 0.000000000000000000, 0.5149999999999917977, 2.350000000000000089 ) ) ;
#5444=ORIENTED_EDGE ( 'NONE', *, *, #3587, .T. ) ;
#5451=ORIENTED_EDGE ( 'NONE', *, *, #1940, .F. ) ;
#5453=CARTESIAN_POINT ( 'NONE',  ( 2.740000000000000213, 0.9838866223910001096, -0.5150000000000001243 ) ) ;
#5466=ADVANCED_FACE ( 'NONE', ( #2016 ), #5693, .T. ) ;
#5468=DIRECTION ( 'NONE',  ( -1.000000000000000000, -0.000000000000000000, -0.000000000000000000 ) ) ;
#5471=ADVANCED_FACE ( 'NONE', ( #631 ), #601, .F. ) ;
#5483=EDGE_CURVE ( 'NONE', #3078, #4039, #247, .T. ) ;
#5491=DIRECTION ( 'NONE',  ( -1.000000000000000000, -0.000000000000000000, -0.000000000000000000 ) ) ;
#5493=ORIENTED_EDGE ( 'NONE', *, *, #4138, .T. ) ;
#5504=ADVANCED_FACE ( 'NONE', ( #692 ), #4383, .F. ) ;
#5506=CARTESIAN_POINT ( 'NONE',  ( 2.740000000000000213, 0.5150000000000035660, -0.9838866223905657904 ) ) ;
#5523=DIRECTION ( 'NONE',  ( -1.000000000000000000, -0.000000000000000000, -0.000000000000000000 ) ) ;
#5529=CARTESIAN_POINT ( 'NONE',  ( 0.06760930072668894231, -0.9010842325122929708, -0.5150000000000000133 ) ) ;
#5532=CARTESIAN_POINT ( 'NONE',  ( 1.794155980045909482, 0.000000000000000000, 0.000000000000000000 ) ) ;
#5535=ORIENTED_EDGE ( 'NONE', *, *, #2019, .T. ) ;
#5541=CARTESIAN_POINT ( 'NONE',  ( 1.849560077140108172, -0.7556913915602447851, 0.5149999999999994582 ) ) ;
#5543=FACE_OUTER_BOUND ( 'NONE', #4633, .T. ) ;
#5545=ORIENTED_EDGE ( 'NONE', *, *, #1617, .F. ) ;
#5546=VECTOR ( 'NONE', #5624, 1000.000000000000114 ) ;
#5550=AXIS2_PLACEMENT_3D ( 'NONE', #5442, #2520, #4872 ) ;
#5555=FACE_OUTER_BOUND ( 'NONE', #3418, .T. ) ;
#5573=ADVANCED_FACE ( 'NONE', ( #2111, #2690 ), #5815, .F. ) ;
#5583=DIRECTION ( 'NONE',  ( -1.000000000000000000, 0.000000000000000000, -0.000000000000000000 ) ) ;
#5605=AXIS2_PLACEMENT_3D ( 'NONE', #4934, #414, #767 ) ;
#5611=STYLED_ITEM('',(#6027),#189);
#5622=CIRCLE ( 'NONE', #2332, 7.983406227920510467 ) ;
#5624=DIRECTION ( 'NONE',  ( 0.8949343913984706411, 1.557891129246106293E-15, -0.4461977533473793778 ) ) ;
#5627=VECTOR ( 'NONE', #3238, 1000.000000000000114 ) ;
#5635=ORIENTED_EDGE ( 'NONE', *, *, #5132, .F. ) ;
#5644=SURFACE_STYLE_FILL_AREA ( #5902 ) ;
#5654=DIRECTION ( 'NONE',  ( -0.8949343913984706411, 0.4461977533473793223, 0.000000000000000000 ) ) ;
#5657=DIRECTION ( 'NONE',  ( 0.4461977533474923430, -0.8949343913984144638, 0.000000000000000000 ) ) ;
#5676=ADVANCED_FACE ( 'NONE', ( #5850 ), #4458, .T. ) ;
#5693=CYLINDRICAL_SURFACE ( 'NONE', #3786, 2.500000000000000000 ) ;
#5706=ORIENTED_EDGE ( 'NONE', *, *, #97, .T. ) ;
#5715=ORIENTED_EDGE ( 'NONE', *, *, #1940, .T. ) ;
#5721=CARTESIAN_POINT ( 'NONE',  ( 2.740000000000000213, -0.5150000000000022338, 0.6774776749089210792 ) ) ;
#5726=CIRCLE ( 'NONE', #887, 7.864440107515430434 ) ;
#5737=DIRECTION ( 'NONE',  ( 0.000000000000000000, 0.000000000000000000, 1.000000000000000000 ) ) ;
#5738=EDGE_CURVE ( 'NONE', #4020, #1770, #1385, .T. ) ;
#5740=( GEOMETRIC_REPRESENTATION_CONTEXT ( 3 ) GLOBAL_UNCERTAINTY_ASSIGNED_CONTEXT ( ( #4494 ) ) GLOBAL_UNIT_ASSIGNED_CONTEXT ( ( #4587, #5423, #4056 ) ) REPRESENTATION_CONTEXT ( 'NONE', 'WORKASPACE' ) );
#5753=ORIENTED_EDGE ( 'NONE', *, *, #5072, .F. ) ;
#5755=CARTESIAN_POINT ( 'NONE',  ( 0.9586399445693768451, 0.5149999999999971267, 0.8293189044373084906 ) ) ;
#5757=CARTESIAN_POINT ( 'NONE',  ( 0.000000000000000000, 0.5150000000000083400, -2.349999999999997424 ) ) ;
#5761=EDGE_CURVE ( 'NONE', #2555, #1563, #2839, .T. ) ;
#5772=ADVANCED_FACE ( 'NONE', ( #5543 ), #1434, .T. ) ;
#5774=DIRECTION ( 'NONE',  ( 1.007709689656716815E-16, 1.000000000000000000, 3.606821995490527259E-15 ) ) ;
#5777=AXIS2_PLACEMENT_3D ( 'NONE', #4740, #4350, #579 ) ;
#5781=AXIS2_PLACEMENT_3D ( 'NONE', #2107, #687, #3058 ) ;
#5784=CARTESIAN_POINT ( 'NONE',  ( 2.740000000000000213, -0.5150000000000034550, 0.9838866223909983333 ) ) ;
#5789=ORIENTED_EDGE ( 'NONE', *, *, #458, .T. ) ;
#5790=EDGE_LOOP ( 'NONE', ( #4198, #4592, #4347, #2144, #1404 ) ) ;
#5802=AXIS2_PLACEMENT_3D ( 'NONE', #5453, #5966, #3661 ) ;
#5810=AXIS2_PLACEMENT_3D ( 'NONE', #1058, #616, #2485 ) ;
#5812=DIRECTION ( 'NONE',  ( 0.000000000000000000, 1.000000000000000000, 0.000000000000000000 ) ) ;
#5814=CARTESIAN_POINT ( 'NONE',  ( 3.016506661494197328, 7.007546303702493782E-17, 0.000000000000000000 ) ) ;
#5815=PLANE ( 'NONE',  #2640 ) ;
#5816=DIRECTION ( 'NONE',  ( 0.000000000000000000, -3.606821995490527259E-15, 1.000000000000000000 ) ) ;
#5821=B_SPLINE_CURVE_WITH_KNOTS ( 'NONE', 3,
 ( #2025, #665, #2181, #3667 ),
 .UNSPECIFIED., .F., .F.,
 ( 4, 4 ),
 ( 0.004656695504653254707, 0.007337072591785142629 ),
 .UNSPECIFIED. ) ;
#5823=AXIS2_PLACEMENT_3D ( 'NONE', #1324, #366, #3089 ) ;
#5831=VERTEX_POINT ( 'NONE', #4123 ) ;
#5840=DIRECTION ( 'NONE',  ( 0.000000000000000000, 0.000000000000000000, 1.000000000000000000 ) ) ;
#5845=( GEOMETRIC_REPRESENTATION_CONTEXT ( 3 ) GLOBAL_UNCERTAINTY_ASSIGNED_CONTEXT ( ( #779 ) ) GLOBAL_UNIT_ASSIGNED_CONTEXT ( ( #1753, #4462, #3574 ) ) REPRESENTATION_CONTEXT ( 'NONE', 'WORKASPACE' ) );
#5850=FACE_OUTER_BOUND ( 'NONE', #4661, .T. ) ;
#5852=ORIENTED_EDGE ( 'NONE', *, *, #4514, .T. ) ;
#5853=ADVANCED_FACE ( 'NONE', ( #1514 ), #4584, .F. ) ;
#5863=ORIENTED_EDGE ( 'NONE', *, *, #1306, .F. ) ;
#5864=FACE_OUTER_BOUND ( 'NONE', #4175, .T. ) ;
#5871=CARTESIAN_POINT ( 'NONE',  ( 2.740000000000000213, 0.5149999999999965716, 0.9838866223910015529 ) ) ;
#5885=CARTESIAN_POINT ( 'NONE',  ( 0.06760930072668894231, 0.9010842325122832008, -0.5150000000000000133 ) ) ;
#5889=ORIENTED_EDGE ( 'NONE', *, *, #565, .T. ) ;
#5892=ORIENTED_EDGE ( 'NONE', *, *, #496, .F. ) ;
#5893=CARTESIAN_POINT ( 'NONE',  ( 8.000000000000000000, -4.896755294805453861E-15, 0.5150000000000000133 ) ) ;
#5896=VECTOR ( 'NONE', #504, 1000.000000000000000 ) ;
#5902=FILL_AREA_STYLE ('',( #783 ) ) ;
#5903=EDGE_CURVE ( 'NONE', #1334, #3605, #123, .T. ) ;
#5916=DIRECTION ( 'NONE',  ( 0.8949343913984706411, -0.4461977533473793778, 0.000000000000000000 ) ) ;
#5917=EDGE_LOOP ( 'NONE', ( #5033, #1689, #350, #1302 ) ) ;
#5929=CARTESIAN_POINT ( 'NONE',  ( 2.740000000000000213, 0.000000000000000000, 0.000000000000000000 ) ) ;
#5934=VECTOR ( 'NONE', #2541, 1000.000000000000114 ) ;
#5941=ORIENTED_EDGE ( 'NONE', *, *, #4810, .T. ) ;
#5945=CONICAL_SURFACE ( 'NONE', #5284, 3077.683537175319998, 1.256637061435923686 ) ;
#5950=APPLICATION_CONTEXT ( 'automotive_design' ) ;
#5966=DIRECTION ( 'NONE',  ( -1.000000000000000000, 0.000000000000000000, -0.000000000000000000 ) ) ;
#6021=COLOUR_RGB('Black',0.12,0.14,0.17);
#6022=FILL_AREA_STYLE_COLOUR('',#6021);
#6023=FILL_AREA_STYLE('',(#6022));
#6024=SURFACE_STYLE_FILL_AREA(#6023);
#6025=SURFACE_SIDE_STYLE('',(#6024));
#6026=SURFACE_STYLE_USAGE(.BOTH.,#6025);
#6027=PRESENTATION_STYLE_ASSIGNMENT((#6026));
ENDSEC;
END-ISO-10303-21;
